ISO-10303-21;
HEADER;
FILE_DESCRIPTION (('STEP AP214'),
    '1' );
FILE_NAME ('hex nut gradec_iso_ISO - 4034 - M10 - N.step',
    '2026-10-10T03:43:58',
    ( '' ),
    ( '' ),
    'SwSTEP 2.0',
    'SolidWorks 2026',
    '' );
FILE_SCHEMA (( 'AUTOMOTIVE_DESIGN' ));
ENDSEC;

DATA;
#124=CYLINDRICAL_SURFACE ( 'NONE', #1949, 5.000000000000000888 ) ;
#126=EDGE_CURVE ( 'NONE', #42836, #57574, #45365, .T. ) ;
#811=AXIS2_PLACEMENT_3D ( 'NONE', #11235, #38319, #43595 ) ;
#902=VERTEX_POINT ( 'NONE', #49437 ) ;
#985=ORIENTED_EDGE ( 'NONE', *, *, #35604, .F. ) ;
#989=VERTEX_POINT ( 'NONE', #6189 ) ;
#997=ORIENTED_EDGE ( 'NONE', *, *, #9206, .T. ) ;
#1036=CARTESIAN_POINT ( 'NONE',  ( 0.6527133886630180903, -8.860760056385778682, -9.003039949738228742 ) ) ;
#1172=VERTEX_POINT ( 'NONE', #37776 ) ;
#1313=VERTEX_POINT ( 'NONE', #43729 ) ;
#1334=EDGE_CURVE ( 'NONE', #10029, #21805, #48601, .T. ) ;
#1400=CARTESIAN_POINT ( 'NONE',  ( 8.000000000000000000, 3.115336682267017210, -0.3193931313915070458 ) ) ;
#1483=CARTESIAN_POINT ( 'NONE',  ( 0.000000000000000000, 0.000000000000000000, 0.000000000000000000 ) ) ;
#1489=CARTESIAN_POINT ( 'NONE',  ( -8.000000000000000000, 4.618802153516996079, -0.7145311798163263006 ) ) ;
#1540=CARTESIAN_POINT ( 'NONE',  ( -1.734723475976807094E-15, 9.237604307034022355, -8.785468820183664818 ) ) ;
#1618=( GEOMETRIC_REPRESENTATION_CONTEXT ( 3 ) GLOBAL_UNCERTAINTY_ASSIGNED_CONTEXT ( ( #3629 ) ) GLOBAL_UNIT_ASSIGNED_CONTEXT ( ( #16852, #59753, #22487 ) ) REPRESENTATION_CONTEXT ( 'NONE', 'WORKASPACE' ) );
#1695=DIRECTION ( 'NONE',  ( 0.000000000000000000, 0.000000000000000000, 1.000000000000000000 ) ) ;
#1721=CARTESIAN_POINT ( 'NONE',  ( -6.183861102004804070E-16, 9.237604307034020579, -9.500000000000000000 ) ) ;
#1949=AXIS2_PLACEMENT_3D ( 'NONE', #32493, #31802, #6093 ) ;
#2093=CARTESIAN_POINT ( 'NONE',  ( 4.000000000000011546, -6.928203230275505220, -9.500000000000000000 ) ) ;
#2181=ADVANCED_FACE ( 'NONE', ( #53171 ), #4657, .F. ) ;
#2201=CARTESIAN_POINT ( 'NONE',  ( -4.680456609903988152, -6.535341423375606418, -9.483111142572225205 ) ) ;
#2238=DIRECTION ( 'NONE',  ( -0.000000000000000000, -0.000000000000000000, 1.000000000000000000 ) ) ;
#2241=ORIENTED_EDGE ( 'NONE', *, *, #35604, .T. ) ;
#2283=CARTESIAN_POINT ( 'NONE',  ( 0.000000000000000000, 0.000000000000000000, -9.474599999999998801 ) ) ;
#2483=CARTESIAN_POINT ( 'NONE',  ( -3.816391647148975608E-14, -9.237604307034022355, -0.7145311798163346273 ) ) ;
#2489=CARTESIAN_POINT ( 'NONE',  ( 3.319543390096045155, -7.321065037175443990, -0.01688885742777720272 ) ) ;
#2598=CARTESIAN_POINT ( 'NONE',  ( 0.6543471694412384965, 8.859816792613651515, -0.4964154566687983272 ) ) ;
#2668=LINE ( 'NONE', #50507, #54840 ) ;
#2669=CARTESIAN_POINT ( 'NONE',  ( 8.000000000000001776, 0.000000000000000000, -9.500000000000000000 ) ) ;
#2679=CARTESIAN_POINT ( 'NONE',  ( -8.000000000000000000, 1.572549600175622730, -9.431055444744870897 ) ) ;
#2994=CARTESIAN_POINT ( 'NONE',  ( -1.313474075707242950, -8.479269695850868871, -0.3167204509598467999 ) ) ;
#3031=EDGE_CURVE ( 'NONE', #1172, #21805, #34299, .T. ) ;
#3089=CIRCLE ( 'NONE', #50229, 8.000000000000000000 ) ;
#3279=ORIENTED_EDGE ( 'NONE', *, *, #10790, .F. ) ;
#3294=DIRECTION ( 'NONE',  ( 0.000000000000000000, 0.000000000000000000, -1.000000000000000000 ) ) ;
#3385=CARTESIAN_POINT ( 'NONE',  ( 4.680456609903976606, 6.535341423375585101, -0.01688885742776517068 ) ) ;
#3629=UNCERTAINTY_MEASURE_WITH_UNIT (LENGTH_MEASURE( 1.000000000000000082E-05 ), #16852, 'distance_accuracy_value', 'NONE');
#3732=DIRECTION ( 'NONE',  ( 1.000000000000000000, 0.000000000000000000, 0.000000000000000000 ) ) ;
#3778=CARTESIAN_POINT ( 'NONE',  ( 0.000000000000000000, 0.000000000000000000, 0.000000000000000000 ) ) ;
#3792=CARTESIAN_POINT ( 'NONE',  ( 0.000000000000000000, 0.000000000000000000, 0.000000000000000000 ) ) ;
#3927=ORIENTED_EDGE ( 'NONE', *, *, #12373, .F. ) ;
#3998=( GEOMETRIC_REPRESENTATION_CONTEXT ( 3 ) GLOBAL_UNCERTAINTY_ASSIGNED_CONTEXT ( ( #41612 ) ) GLOBAL_UNIT_ASSIGNED_CONTEXT ( ( #41278, #57115, #8928 ) ) REPRESENTATION_CONTEXT ( 'NONE', 'WORKASPACE' ) );
#4013=ORIENTED_EDGE ( 'NONE', *, *, #1334, .F. ) ;
#4147=ORIENTED_EDGE ( 'NONE', *, *, #28779, .T. ) ;
#4273=CARTESIAN_POINT ( 'NONE',  ( 0.000000000000000000, 0.000000000000000000, -9.500000000000000000 ) ) ;
#4328=DIRECTION ( 'NONE',  ( -1.000000000000000000, 0.000000000000000000, 0.000000000000000000 ) ) ;
#4449=ORIENTED_EDGE ( 'NONE', *, *, #37207, .T. ) ;
#4657=PLANE ( 'NONE',  #54285 ) ;
#4789=AXIS2_PLACEMENT_3D ( 'NONE', #65321, #38580, #60026 ) ;
#4946=CARTESIAN_POINT ( 'NONE',  ( -2.309976723937615439, 7.903938623646864059, -0.1306530452038096035 ) ) ;
#4998=EDGE_CURVE ( 'NONE', #1313, #29309, #26242, .T. ) ;
#5007=SURFACE_STYLE_USAGE ( .BOTH. , #65054 ) ;
#5132=AXIS2_PLACEMENT_3D ( 'NONE', #56450, #51868, #41661 ) ;
#5183=EDGE_CURVE ( 'NONE', #902, #36668, #9118, .T. ) ;
#5276=CIRCLE ( 'NONE', #45711, 4.250000000000000000 ) ;
#5379=CARTESIAN_POINT ( 'NONE',  ( 0.000000000000000000, 9.237604307034020579, 0.000000000000000000 ) ) ;
#5453=CARTESIAN_POINT ( 'NONE',  ( -8.000000000000000000, 1.572549600175613627, -0.06894455525513029648 ) ) ;
#5538=CARTESIAN_POINT ( 'NONE',  ( 8.000000000000000000, -3.098204225878180118, -9.184209322808124298 ) ) ;
#5629=CARTESIAN_POINT ( 'NONE',  ( -8.000000000000000000, 4.618802153516996079, -9.500000000000000000 ) ) ;
#5925=EDGE_LOOP ( 'NONE', ( #43965, #40597, #32006 ) ) ;
#6035=VECTOR ( 'NONE', #36197, 1000.000000000000000 ) ;
#6093=DIRECTION ( 'NONE',  ( 1.000000000000000000, 0.000000000000000000, 0.000000000000000000 ) ) ;
#6105=EDGE_CURVE ( 'NONE', #33757, #8652, #8374, .T. ) ;
#6109=CARTESIAN_POINT ( 'NONE',  ( -8.000000000000000000, 4.618802153516996079, -0.7145311798163263006 ) ) ;
#6163=ORIENTED_EDGE ( 'NONE', *, *, #4998, .F. ) ;
#6189=CARTESIAN_POINT ( 'NONE',  ( 5.000000000000000888, 6.123233995736767268E-16, -9.474599999999998801 ) ) ;
#6289=AXIS2_PLACEMENT_3D ( 'NONE', #60274, #2238, #7521 ) ;
#6443=CARTESIAN_POINT ( 'NONE',  ( 5.690023276062394331, 5.952467836904149934, -9.369346954796190730 ) ) ;
#6467=DIRECTION ( 'NONE',  ( 0.000000000000000000, -0.000000000000000000, 1.000000000000000000 ) ) ;
#6488=CARTESIAN_POINT ( 'NONE',  ( -8.000000000000000000, -3.867591403079189583, -9.002324684675413025 ) ) ;
#6695=CARTESIAN_POINT ( 'NONE',  ( 6.686525924292799239, -5.377136764700172655, -0.3167204509598466888 ) ) ;
#6791=ORIENTED_EDGE ( 'NONE', *, *, #24005, .T. ) ;
#7001=CARTESIAN_POINT ( 'NONE',  ( -4.000000000000009770, -6.928203230275505220, -9.500000000000000000 ) ) ;
#7027=CARTESIAN_POINT ( 'NONE',  ( 8.000000000000000000, 1.572549600175624063, -0.06894455525513173977 ) ) ;
#7031=LINE ( 'NONE', #30231, #38423 ) ;
#7032=LINE ( 'NONE', #5629, #47556 ) ;
#7067=CARTESIAN_POINT ( 'NONE',  ( 5.000000000000000888, 0.000000000000000000, -25.03750572909317285 ) ) ;
#7091=DIRECTION ( 'NONE',  ( 1.000000000000000000, 0.000000000000000000, 0.000000000000000000 ) ) ;
#7116=CARTESIAN_POINT ( 'NONE',  ( -7.345652830558763391, 4.996589667937367807, -0.4964154566687925541 ) ) ;
#7167=B_SPLINE_CURVE_WITH_KNOTS ( 'NONE', 3,
 ( #43265, #11611, #6695, #16891, #59451, #54515 ),
 .UNSPECIFIED., .F., .F.,
 ( 4, 2, 4 ),
 ( 2.380731629547626167E-07, 0.002336973833157547729, 0.004673709593152140102 ),
 .UNSPECIFIED. ) ;
#7225=ORIENTED_EDGE ( 'NONE', *, *, #31683, .T. ) ;
#7270=DIRECTION ( 'NONE',  ( 0.000000000000000000, 0.000000000000000000, 1.000000000000000000 ) ) ;
#7481=CARTESIAN_POINT ( 'NONE',  ( -6.686525924292793022, 5.377136764700151339, -0.3167204509598375850 ) ) ;
#7482=VERTEX_POINT ( 'NONE', #2483 ) ;
#7521=DIRECTION ( 'NONE',  ( 1.000000000000000000, 0.000000000000000000, 0.000000000000000000 ) ) ;
#7532=CARTESIAN_POINT ( 'NONE',  ( 3.318518101603014525, 7.321656987762867885, -9.500000000000005329 ) ) ;
#7629=FACE_OUTER_BOUND ( 'NONE', #68479, .T. ) ;
#7664=FACE_OUTER_BOUND ( 'NONE', #66882, .T. ) ;
#7724=DIRECTION ( 'NONE',  ( -1.000000000000000000, 0.000000000000000000, 0.000000000000000000 ) ) ;
#7757=ORIENTED_EDGE ( 'NONE', *, *, #62641, .T. ) ;
#7821=EDGE_CURVE ( 'NONE', #58090, #989, #27627, .T. ) ;
#7963=CARTESIAN_POINT ( 'NONE',  ( -8.000000000000000000, -4.618802153517023612, -9.500000000000000000 ) ) ;
#8040=CARTESIAN_POINT ( 'NONE',  ( -5.000000000000000888, 6.123233995736767268E-16, -25.03750572909317285 ) ) ;
#8043=ORIENTED_EDGE ( 'NONE', *, *, #46385, .T. ) ;
#8216=CARTESIAN_POINT ( 'NONE',  ( 4.250000000000000000, 0.000000000000000000, -8.949444346342716017 ) ) ;
#8250=ORIENTED_EDGE ( 'NONE', *, *, #19133, .F. ) ;
#8319=DIRECTION ( 'NONE',  ( 1.000000000000000000, 0.000000000000000000, 0.000000000000000000 ) ) ;
#8374=CIRCLE ( 'NONE', #55557, 8.000000000000001776 ) ;
#8511=EDGE_CURVE ( 'NONE', #45082, #39183, #10814, .T. ) ;
#8545=CARTESIAN_POINT ( 'NONE',  ( -8.000000000000000000, -4.618802153517024500, -0.7145311798163346273 ) ) ;
#8652=VERTEX_POINT ( 'NONE', #16756 ) ;
#8686=DIRECTION ( 'NONE',  ( 0.000000000000000000, 0.000000000000000000, 1.000000000000000000 ) ) ;
#8733=DIRECTION ( 'NONE',  ( -0.000000000000000000, 0.000000000000000000, -1.000000000000000000 ) ) ;
#8928=( NAMED_UNIT ( * ) SI_UNIT ( $, .STERADIAN. ) SOLID_ANGLE_UNIT ( ) );
#8979=EDGE_CURVE ( 'NONE', #36166, #52636, #64744, .T. ) ;
#9106=CARTESIAN_POINT ( 'NONE',  ( 0.000000000000000000, 0.000000000000000000, -9.500000000000000000 ) ) ;
#9118=LINE ( 'NONE', #14731, #6035 ) ;
#9174=CARTESIAN_POINT ( 'NONE',  ( -8.000000000000000000, -4.618802153517024500, -0.7145311798163346273 ) ) ;
#9206=EDGE_CURVE ( 'NONE', #31187, #31627, #22349, .T. ) ;
#9328=CARTESIAN_POINT ( 'NONE',  ( 8.000000000000000000, 3.115336682267014101, -9.180606868608490956 ) ) ;
#9536=EDGE_CURVE ( 'NONE', #36166, #989, #60072, .T. ) ;
#9549=FACE_OUTER_BOUND ( 'NONE', #68436, .T. ) ;
#9595=DIRECTION ( 'NONE',  ( 0.000000000000000000, 0.000000000000000000, 1.000000000000000000 ) ) ;
#9745=ADVANCED_FACE ( 'NONE', ( #20987 ), #38953, .T. ) ;
#9753=ORIENTED_EDGE ( 'NONE', *, *, #48332, .T. ) ;
#9815=AXIS2_PLACEMENT_3D ( 'NONE', #62416, #68714, #42338 ) ;
#9817=AXIS2_PLACEMENT_3D ( 'NONE', #20749, #62637, #41866 ) ;
#9861=FACE_OUTER_BOUND ( 'NONE', #53704, .T. ) ;
#9887=EDGE_LOOP ( 'NONE', ( #40031, #63016, #43313 ) ) ;
#9986=FACE_OUTER_BOUND ( 'NONE', #45980, .T. ) ;
#9991=PRODUCT_DEFINITION ( 'UNKNOWN', '', #23172, #27497 ) ;
#10029=VERTEX_POINT ( 'NONE', #68730 ) ;
#10039=CARTESIAN_POINT ( 'NONE',  ( 6.689127551062003185, 5.375634714784618851, -0.3173508448886520061 ) ) ;
#10049=DIRECTION ( 'NONE',  ( -0.000000000000000000, -0.000000000000000000, 1.000000000000000000 ) ) ;
#10100=FACE_OUTER_BOUND ( 'NONE', #44750, .T. ) ;
#10139=ORIENTED_EDGE ( 'NONE', *, *, #18850, .F. ) ;
#10205=ADVANCED_FACE ( 'NONE', ( #37412 ), #124, .F. ) ;
#10618=EDGE_CURVE ( 'NONE', #59496, #39183, #18860, .T. ) ;
#10662=CARTESIAN_POINT ( 'NONE',  ( -4.681481898397003683, 6.534749472788141667, -9.500000000000005329 ) ) ;
#10790=EDGE_CURVE ( 'NONE', #56693, #989, #30178, .T. ) ;
#10814=CIRCLE ( 'NONE', #11971, 8.000000000000000000 ) ;
#10940=AXIS2_PLACEMENT_3D ( 'NONE', #11016, #37398, #28235 ) ;
#10964=DIRECTION ( 'NONE',  ( 0.000000000000000000, -0.000000000000000000, 1.000000000000000000 ) ) ;
#10971=ORIENTED_EDGE ( 'NONE', *, *, #63782, .F. ) ;
#10976=ORIENTED_EDGE ( 'NONE', *, *, #21815, .F. ) ;
#11016=CARTESIAN_POINT ( 'NONE',  ( 0.000000000000000000, 0.000000000000000000, -9.500000000000000000 ) ) ;
#11081=ORIENTED_EDGE ( 'NONE', *, *, #5183, .F. ) ;
#11219=AXIS2_PLACEMENT_3D ( 'NONE', #57524, #29747, #30792 ) ;
#11235=CARTESIAN_POINT ( 'NONE',  ( 0.000000000000000000, 0.000000000000000000, -9.500000000000000000 ) ) ;
#11242=EDGE_CURVE ( 'NONE', #52636, #58090, #2668, .T. ) ;
#11249=CARTESIAN_POINT ( 'NONE',  ( -3.660532965668827021, 7.124194613927616437, 6.003346013664852075E-15 ) ) ;
#11255=EDGE_LOOP ( 'NONE', ( #61520, #57948, #35538, #31993 ) ) ;
#11588=CARTESIAN_POINT ( 'NONE',  ( 8.000000000000000000, 3.871967595402137530, -0.4989386132324603595 ) ) ;
#11595=DIRECTION ( 'NONE',  ( -0.000000000000000000, 0.000000000000000000, -1.000000000000000000 ) ) ;
#11600=EDGE_CURVE ( 'NONE', #42836, #44487, #30511, .T. ) ;
#11611=CARTESIAN_POINT ( 'NONE',  ( 7.345652830558766055, -4.996589667937388235, -0.4964154566688021020 ) ) ;
#11693=ORIENTED_EDGE ( 'NONE', *, *, #24005, .F. ) ;
#11769=CARTESIAN_POINT ( 'NONE',  ( -8.000000000000000000, 3.115336682266996338, -0.3193931313915024384 ) ) ;
#11817=ORIENTED_EDGE ( 'NONE', *, *, #59760, .F. ) ;
#11828=B_SPLINE_CURVE_WITH_KNOTS ( 'NONE', 3,
 ( #1540, #44807, #44085, #66285, #7532, #39187 ),
 .UNSPECIFIED., .F., .F.,
 ( 4, 2, 4 ),
 ( 2.380731629557410192E-07, 0.002336973833157566377, 0.004673709593152176531 ),
 .UNSPECIFIED. ) ;
#11835=CARTESIAN_POINT ( 'NONE',  ( -8.000000000000000000, 4.618802153517024500, -8.785468820183664818 ) ) ;
#11836=ADVANCED_FACE ( 'NONE', ( #9861 ), #32254, .F. ) ;
#11848=CARTESIAN_POINT ( 'NONE',  ( -4.000000000000009770, -6.928203230275505220, 0.000000000000000000 ) ) ;
#11851=ORIENTED_EDGE ( 'NONE', *, *, #35357, .T. ) ;
#11927=CARTESIAN_POINT ( 'NONE',  ( -2.645508037661904233, -7.710219529346618472, -9.431901280394557219 ) ) ;
#11951=CIRCLE ( 'NONE', #69290, 8.000000000000000000 ) ;
#11953=CARTESIAN_POINT ( 'NONE',  ( 8.000000000000000000, 4.618802153517024500, -0.7145311798163346273 ) ) ;
#11971=AXIS2_PLACEMENT_3D ( 'NONE', #3792, #57263, #13652 ) ;
#12067=CARTESIAN_POINT ( 'NONE',  ( 5.355005115540897975, 6.145890662064648069, -9.417753204360288066 ) ) ;
#12107=B_SPLINE_CURVE_WITH_KNOTS ( 'NONE', 3,
 ( #24105, #41651, #2994, #24792, #50822, #62769 ),
 .UNSPECIFIED., .F., .F.,
 ( 4, 2, 4 ),
 ( 2.380731630023936087E-07, 0.002336973833157593699, 0.004673709593152186939 ),
 .UNSPECIFIED. ) ;
#12157=CARTESIAN_POINT ( 'NONE',  ( 8.000000000000003553, -4.618802153517020948, -0.7145311798163346273 ) ) ;
#12171=CARTESIAN_POINT ( 'NONE',  ( 4.000000000000011546, -6.928203230275505220, -9.500000000000000000 ) ) ;
#12200=DIRECTION ( 'NONE',  ( -0.5000000000000012212, -0.8660254037844380415, 0.000000000000000000 ) ) ;
#12251=CARTESIAN_POINT ( 'NONE',  ( 5.000000000000000888, 6.123233995736767268E-16, -9.474599999999998801 ) ) ;
#12277=DIRECTION ( 'NONE',  ( -0.000000000000000000, -0.000000000000000000, 1.000000000000000000 ) ) ;
#12373=EDGE_CURVE ( 'NONE', #38945, #39183, #25551, .T. ) ;
#12419=CARTESIAN_POINT ( 'NONE',  ( 4.680456609903976606, 6.535341423375584213, -9.483111142572232310 ) ) ;
#12511=ORIENTED_EDGE ( 'NONE', *, *, #46833, .F. ) ;
#12818=CARTESIAN_POINT ( 'NONE',  ( -8.000000000000000000, -0.7805016046291022302, -9.500000000000003553 ) ) ;
#12926=EDGE_LOOP ( 'NONE', ( #24749, #49931, #4449, #16861, #54293, #15648 ) ) ;
#13242=AXIS2_PLACEMENT_3D ( 'NONE', #32753, #27119, #21844 ) ;
#13248=DIRECTION ( 'NONE',  ( 0.8660254037844379305, -0.5000000000000011102, 0.000000000000000000 ) ) ;
#13375=FACE_BOUND ( 'NONE', #53664, .T. ) ;
#13458=ORIENTED_EDGE ( 'NONE', *, *, #22384, .F. ) ;
#13531=CARTESIAN_POINT ( 'NONE',  ( -6.689127551062013843, -5.375634714784636614, -0.3173508448886639410 ) ) ;
#13585=CARTESIAN_POINT ( 'NONE',  ( -4.174999999999999822, 5.112900386440199535E-16, -0.5776712190230133270 ) ) ;
#13589=ORIENTED_EDGE ( 'NONE', *, *, #21971, .T. ) ;
#13652=DIRECTION ( 'NONE',  ( -1.000000000000000000, 0.000000000000000000, 0.000000000000000000 ) ) ;
#13711=PLANE ( 'NONE',  #28295 ) ;
#13781=CARTESIAN_POINT ( 'NONE',  ( -6.689127551062009402, -5.375634714784637502, -9.182649155111338501 ) ) ;
#13860=FACE_OUTER_BOUND ( 'NONE', #31882, .T. ) ;
#14007=FACE_OUTER_BOUND ( 'NONE', #11255, .T. ) ;
#14034=ADVANCED_FACE ( 'NONE', ( #10100 ), #36492, .T. ) ;
#14080=CONICAL_SURFACE ( 'NONE', #62385, 8.000000000000001776, 1.047197551196595855 ) ;
#14367=ADVANCED_FACE ( 'NONE', ( #41349 ), #36067, .T. ) ;
#14413=CARTESIAN_POINT ( 'NONE',  ( -4.999999999999999112, 6.123233995736765296E-16, 3.469446951953614189E-15 ) ) ;
#14418=AXIS2_PLACEMENT_3D ( 'NONE', #1483, #15925, #37371 ) ;
#14497=CARTESIAN_POINT ( 'NONE',  ( -5.000000000000000888, 0.000000000000000000, -9.474599999999998801 ) ) ;
#14585=ORIENTED_EDGE ( 'NONE', *, *, #10790, .T. ) ;
#14598=ORIENTED_EDGE ( 'NONE', *, *, #7821, .F. ) ;
#14619=AXIS2_PLACEMENT_3D ( 'NONE', #18368, #50719, #19059 ) ;
#14665=CARTESIAN_POINT ( 'NONE',  ( 5.007715329123879543E-16, -9.237604307034043671, -9.500000000000000000 ) ) ;
#14731=CARTESIAN_POINT ( 'NONE',  ( 4.174999999999999822, 0.000000000000000000, -0.5776712190230133270 ) ) ;
#14788=CARTESIAN_POINT ( 'NONE',  ( -8.000000000000000000, -0.7805016046291012310, 1.011357339021634605E-15 ) ) ;
#14861=FACE_OUTER_BOUND ( 'NONE', #12926, .T. ) ;
#14941=AXIS2_PLACEMENT_3D ( 'NONE', #17722, #6467, #34251 ) ;
#14978=VECTOR ( 'NONE', #24229, 1000.000000000000000 ) ;
#15135=ORIENTED_EDGE ( 'NONE', *, *, #31067, .F. ) ;
#15291=DIRECTION ( 'NONE',  ( -0.000000000000000000, -0.000000000000000000, 1.000000000000000000 ) ) ;
#15322=DIRECTION ( 'NONE',  ( -1.000000000000000000, 0.000000000000000000, 0.000000000000000000 ) ) ;
#15329=ADVANCED_FACE ( 'NONE', ( #7629 ), #29081, .T. ) ;
#15364=DIRECTION ( 'NONE',  ( 0.000000000000000000, 0.000000000000000000, -1.000000000000000000 ) ) ;
#15523=CARTESIAN_POINT ( 'NONE',  ( -1.734723475976807094E-15, 9.237604307034022355, -0.7145311798163346273 ) ) ;
#15542=CARTESIAN_POINT ( 'NONE',  ( -3.319543390096040714, 7.321065037175420898, -9.483111142572234087 ) ) ;
#15573=SURFACE_STYLE_FILL_AREA ( #63765 ) ;
#15606=EDGE_LOOP ( 'NONE', ( #7757, #50618, #65105 ) ) ;
#15636=VERTEX_POINT ( 'NONE', #8545 ) ;
#15648=ORIENTED_EDGE ( 'NONE', *, *, #3031, .F. ) ;
#15719=CONICAL_SURFACE ( 'NONE', #32590, 5.000000000000000888, 0.9599310885968810325 ) ;
#15844=DIRECTION ( 'NONE',  ( 1.000000000000000000, 0.000000000000000000, 0.000000000000000000 ) ) ;
#15878=CONICAL_SURFACE ( 'NONE', #43987, 8.000000000000001776, 1.047197551196595855 ) ;
#15887=AXIS2_PLACEMENT_3D ( 'NONE', #16677, #23008, #38848 ) ;
#15925=DIRECTION ( 'NONE',  ( 0.000000000000000000, 0.000000000000000000, -1.000000000000000000 ) ) ;
#15959=ADVANCED_FACE ( 'NONE', ( #24212 ), #53985, .T. ) ;
#16195=ORIENTED_EDGE ( 'NONE', *, *, #56861, .F. ) ;
#16207=ORIENTED_EDGE ( 'NONE', *, *, #6105, .T. ) ;
#16383=AXIS2_PLACEMENT_3D ( 'NONE', #63730, #41919, #47876 ) ;
#16677=CARTESIAN_POINT ( 'NONE',  ( 0.000000000000000000, 0.000000000000000000, -9.500000000000000000 ) ) ;
#16751=DIRECTION ( 'NONE',  ( 0.000000000000000000, 0.000000000000000000, -1.000000000000000000 ) ) ;
#16755=ORIENTED_EDGE ( 'NONE', *, *, #1334, .T. ) ;
#16756=CARTESIAN_POINT ( 'NONE',  ( 4.000000000000012434, 6.928203230275504332, -9.500000000000000000 ) ) ;
#16769=EDGE_LOOP ( 'NONE', ( #50665, #59415, #63120, #56351, #10971, #17725 ) ) ;
#16804=CARTESIAN_POINT ( 'NONE',  ( 0.000000000000000000, 0.000000000000000000, 3.469446951953614189E-15 ) ) ;
#16852=( LENGTH_UNIT ( ) NAMED_UNIT ( * ) SI_UNIT ( .MILLI., .METRE. ) );
#16861=ORIENTED_EDGE ( 'NONE', *, *, #55163, .F. ) ;
#16891=CARTESIAN_POINT ( 'NONE',  ( 5.354491962338135735, -6.146186931204420389, -0.06809871960543693870 ) ) ;
#17013=CARTESIAN_POINT ( 'NONE',  ( -8.000000000000001776, 0.000000000000000000, 0.000000000000000000 ) ) ;
#17240=EDGE_CURVE ( 'NONE', #8652, #10029, #46217, .T. ) ;
#17325=VERTEX_POINT ( 'NONE', #17013 ) ;
#17393=CARTESIAN_POINT ( 'NONE',  ( -8.000000000000000000, 3.871967595402113105, -0.4989386132324536427 ) ) ;
#17558=CARTESIAN_POINT ( 'NONE',  ( 3.660532965668831462, -7.124194613927639530, -9.499999999999994671 ) ) ;
#17675=CARTESIAN_POINT ( 'NONE',  ( -4.681481898397006347, 6.534749472788140778, 5.780152832063345514E-15 ) ) ;
#17722=CARTESIAN_POINT ( 'NONE',  ( 0.000000000000000000, 0.000000000000000000, -9.500000000000000000 ) ) ;
#17725=ORIENTED_EDGE ( 'NONE', *, *, #19769, .F. ) ;
#17912=CARTESIAN_POINT ( 'NONE',  ( 1.310872448937988821, -8.480771745766432446, -9.182649155111331396 ) ) ;
#17992=CARTESIAN_POINT ( 'NONE',  ( 4.681481898397010788, -6.534749472788160318, -9.499999999999994671 ) ) ;
#18368=CARTESIAN_POINT ( 'NONE',  ( 0.000000000000000000, 0.000000000000000000, 0.000000000000000000 ) ) ;
#18514=LINE ( 'NONE', #33312, #55494 ) ;
#18583=ADVANCED_FACE ( 'NONE', ( #24526 ), #66432, .T. ) ;
#18584=ORIENTED_EDGE ( 'NONE', *, *, #49564, .F. ) ;
#18634=EDGE_LOOP ( 'NONE', ( #57150, #997, #27031 ) ) ;
#18719=CARTESIAN_POINT ( 'NONE',  ( -7.347286611336974360, -4.995646404165295706, -9.003039949738241177 ) ) ;
#18776=CARTESIAN_POINT ( 'NONE',  ( 3.318518101603014525, 7.321656987762867885, 5.929230630780102373E-15 ) ) ;
#18802=CARTESIAN_POINT ( 'NONE',  ( -5.355005115540905969, -6.145890662064667609, -0.08224679563972382701 ) ) ;
#18850=EDGE_CURVE ( 'NONE', #29309, #15636, #44871, .T. ) ;
#18860=CIRCLE ( 'NONE', #13242, 8.000000000000001776 ) ;
#19009=CARTESIAN_POINT ( 'NONE',  ( 2.309976723937611442, -7.903938623646888928, -0.1306530452038232315 ) ) ;
#19059=DIRECTION ( 'NONE',  ( -1.000000000000000000, 0.000000000000000000, 0.000000000000000000 ) ) ;
#19113=CARTESIAN_POINT ( 'NONE',  ( 4.000000000000012434, 6.928203230275504332, 0.000000000000000000 ) ) ;
#19122=SHAPE_REPRESENTATION_RELATIONSHIP ( 'NONE' , 'NONE' ,  #50551, #49175 ) ;
#19133=EDGE_CURVE ( 'NONE', #31627, #1172, #23072, .T. ) ;
#19230=ADVANCED_FACE ( 'NONE', ( #9549 ), #15878, .T. ) ;
#19405=CIRCLE ( 'NONE', #4789, 8.000000000000000000 ) ;
#19569=CARTESIAN_POINT ( 'NONE',  ( 0.000000000000000000, 0.000000000000000000, -9.500000000000000000 ) ) ;
#19719=EDGE_CURVE ( 'NONE', #7482, #29309, #12107, .T. ) ;
#19733=ORIENTED_EDGE ( 'NONE', *, *, #53481, .T. ) ;
#19738=PRODUCT ( 'hex nut gradec_iso_ISO - 4034 - M10 - N', 'hex nut gradec_iso_ISO - 4034 - M10 - N', '', ( #62832 ) ) ;
#19769=EDGE_CURVE ( 'NONE', #69223, #10029, #63315, .T. ) ;
#19841=CARTESIAN_POINT ( 'NONE',  ( -5.690023276062404101, -5.952467836904166809, -0.1306530452038198453 ) ) ;
#19880=DIRECTION ( 'NONE',  ( 1.000000000000000000, 0.000000000000000000, 0.000000000000000000 ) ) ;
#19888=CARTESIAN_POINT ( 'NONE',  ( 8.000000000000000000, 1.572549600175622952, -9.431055444744870897 ) ) ;
#19913=CARTESIAN_POINT ( 'NONE',  ( 7.347286611336963702, 4.995646404165275278, -0.4969600502617484983 ) ) ;
#19940=DIRECTION ( 'NONE',  ( 0.000000000000000000, 0.000000000000000000, -1.000000000000000000 ) ) ;
#19985=CYLINDRICAL_SURFACE ( 'NONE', #36329, 4.250000000000000000 ) ;
#20290=DIRECTION ( 'NONE',  ( -1.000000000000000000, 0.000000000000000000, 0.000000000000000000 ) ) ;
#20414=EDGE_CURVE ( 'NONE', #36166, #902, #43540, .T. ) ;
#20415=VECTOR ( 'NONE', #40095, 1000.000000000000000 ) ;
#20527=CARTESIAN_POINT ( 'NONE',  ( -6.686525924292787693, 5.377136764700155780, -9.183279549040166856 ) ) ;
#20562=EDGE_CURVE ( 'NONE', #31187, #7482, #36822, .T. ) ;
#20587=DIRECTION ( 'NONE',  ( -0.000000000000000000, -0.000000000000000000, 1.000000000000000000 ) ) ;
#20671=ORIENTED_EDGE ( 'NONE', *, *, #8979, .T. ) ;
#20742=CIRCLE ( 'NONE', #30901, 5.000000000000000888 ) ;
#20749=CARTESIAN_POINT ( 'NONE',  ( 0.000000000000000000, 0.000000000000000000, -0.5776712190230133270 ) ) ;
#20879=DIRECTION ( 'NONE',  ( -1.000000000000000000, 0.000000000000000000, 0.000000000000000000 ) ) ;
#20984=VERTEX_POINT ( 'NONE', #39000 ) ;
#20987=FACE_OUTER_BOUND ( 'NONE', #5925, .T. ) ;
#21180=ORIENTED_EDGE ( 'NONE', *, *, #19133, .T. ) ;
#21232=CARTESIAN_POINT ( 'NONE',  ( -7.345652830558753621, 4.996589667937373136, -9.003584543331209389 ) ) ;
#21369=CARTESIAN_POINT ( 'NONE',  ( 8.000000000000001776, -3.867591403079185142, -9.002324684675414801 ) ) ;
#21398=CIRCLE ( 'NONE', #52829, 4.250000000000000000 ) ;
#21462=CARTESIAN_POINT ( 'NONE',  ( -1.310872448937999701, 8.480771745766400471, -0.3173508448886568911 ) ) ;
#21543=DIRECTION ( 'NONE',  ( 0.000000000000000000, 0.000000000000000000, -1.000000000000000000 ) ) ;
#21731=EDGE_CURVE ( 'NONE', #33757, #61707, #68877, .T. ) ;
#21742=CARTESIAN_POINT ( 'NONE',  ( 4.250000000000000000, 0.000000000000000000, -9.500000000000000000 ) ) ;
#21790=VERTEX_POINT ( 'NONE', #6109 ) ;
#21805=VERTEX_POINT ( 'NONE', #59917 ) ;
#21806=CARTESIAN_POINT ( 'NONE',  ( -4.000000000000013323, 6.928203230275504332, 0.000000000000000000 ) ) ;
#21815=EDGE_CURVE ( 'NONE', #47318, #8652, #11828, .T. ) ;
#21844=DIRECTION ( 'NONE',  ( 1.000000000000000000, 0.000000000000000000, 0.000000000000000000 ) ) ;
#21866=DIRECTION ( 'NONE',  ( 1.000000000000000000, 0.000000000000000000, 0.000000000000000000 ) ) ;
#21971=EDGE_CURVE ( 'NONE', #47318, #38945, #45677, .T. ) ;
#21977=CARTESIAN_POINT ( 'NONE',  ( -3.816391647148975608E-14, -9.237604307034022355, -8.785468820183664818 ) ) ;
#22067=CARTESIAN_POINT ( 'NONE',  ( 7.999999999999998224, -1.555946510856144993, -9.432911297836643172 ) ) ;
#22161=ORIENTED_EDGE ( 'NONE', *, *, #10618, .T. ) ;
#22226=ADVANCED_FACE ( 'NONE', ( #14007 ), #19985, .F. ) ;
#22258=ORIENTED_EDGE ( 'NONE', *, *, #35357, .F. ) ;
#22349=B_SPLINE_CURVE_WITH_KNOTS ( 'NONE', 3,
 ( #65757, #60466, #27749, #11927, #33398, #7001 ),
 .UNSPECIFIED., .F., .F.,
 ( 4, 2, 4 ),
 ( 2.380731630024181461E-07, 0.002336973833157594133, 0.004673709593152186939 ),
 .UNSPECIFIED. ) ;
#22380=DIRECTION ( 'NONE',  ( 1.000000000000000000, 0.000000000000000000, 0.000000000000000000 ) ) ;
#22384=EDGE_CURVE ( 'NONE', #52636, #20984, #18514, .T. ) ;
#22396=EDGE_CURVE ( 'NONE', #21805, #69223, #38757, .T. ) ;
#22487=( NAMED_UNIT ( * ) SI_UNIT ( $, .STERADIAN. ) SOLID_ANGLE_UNIT ( ) );
#22568=FACE_OUTER_BOUND ( 'NONE', #60609, .T. ) ;
#23008=DIRECTION ( 'NONE',  ( 0.000000000000000000, -0.000000000000000000, 1.000000000000000000 ) ) ;
#23072=B_SPLINE_CURVE_WITH_KNOTS ( 'NONE', 3,
 ( #29610, #45092, #2201, #61628, #23998, #13781, #18719, #61283 ),
 .UNSPECIFIED., .F., .F.,
 ( 4, 2, 2, 4 ),
 ( 0.004673709593152186939, 0.005837709341827668555, 0.007001709090503151038, 0.009329708587854118607 ),
 .UNSPECIFIED. ) ;
#23172=PRODUCT_DEFINITION_FORMATION_WITH_SPECIFIED_SOURCE ( 'ANY', '', #19738, .NOT_KNOWN. ) ;
#23195=CARTESIAN_POINT ( 'NONE',  ( 2.309976723937610554, -7.903938623646890704, -9.369346954796176519 ) ) ;
#23276=CARTESIAN_POINT ( 'NONE',  ( 4.000000000000011546, -6.928203230275505220, -9.500000000000000000 ) ) ;
#23309=CARTESIAN_POINT ( 'NONE',  ( -4.000000000000013323, 6.928203230275504332, 0.000000000000000000 ) ) ;
#23327=CIRCLE ( 'NONE', #10940, 8.000000000000000000 ) ;
#23394=B_SPLINE_CURVE_WITH_KNOTS ( 'NONE', 3,
 ( #2093, #17558, #49906, #33042, #23195, #17912, #1036, #39027 ),
 .UNSPECIFIED., .F., .F.,
 ( 4, 2, 2, 4 ),
 ( 0.004673709593152140102, 0.005837709341827639932, 0.007001709090503139762, 0.009329708587854139423 ),
 .UNSPECIFIED. ) ;
#23498=DIRECTION ( 'NONE',  ( 1.000000000000000000, 0.000000000000000000, 0.000000000000000000 ) ) ;
#23897=DIRECTION ( 'NONE',  ( 0.000000000000000000, -0.000000000000000000, 1.000000000000000000 ) ) ;
#23943=CARTESIAN_POINT ( 'NONE',  ( 2.644994884459113571, -7.710515798486386352, -0.08224679563972556173 ) ) ;
#23998=CARTESIAN_POINT ( 'NONE',  ( -5.690023276062404101, -5.952467836904166809, -9.369346954796180071 ) ) ;
#24005=EDGE_CURVE ( 'NONE', #39183, #29751, #51075, .T. ) ;
#24105=CARTESIAN_POINT ( 'NONE',  ( -3.816391647148975608E-14, -9.237604307034022355, -0.7145311798163346273 ) ) ;
#24212=FACE_OUTER_BOUND ( 'NONE', #63064, .T. ) ;
#24229=DIRECTION ( 'NONE',  ( 0.000000000000000000, 0.000000000000000000, 1.000000000000000000 ) ) ;
#24347=DIRECTION ( 'NONE',  ( 1.000000000000000000, 0.000000000000000000, 0.000000000000000000 ) ) ;
#24441=CARTESIAN_POINT ( 'NONE',  ( -4.339467034331206285, -6.732211846623409102, -6.390228312323252966E-15 ) ) ;
#24526=FACE_OUTER_BOUND ( 'NONE', #53354, .T. ) ;
#24605=ORIENTED_EDGE ( 'NONE', *, *, #9536, .F. ) ;
#24657=ORIENTED_EDGE ( 'NONE', *, *, #20414, .T. ) ;
#24749=ORIENTED_EDGE ( 'NONE', *, *, #31067, .T. ) ;
#24762=PLANE ( 'NONE',  #43070 ) ;
#24792=CARTESIAN_POINT ( 'NONE',  ( -2.645508037661902456, -7.710219529346618472, -0.06809871960543704972 ) ) ;
#24834=LINE ( 'NONE', #13585, #63778 ) ;
#24870=ADVANCED_FACE ( 'NONE', ( #36792 ), #14080, .T. ) ;
#24906=DIRECTION ( 'NONE',  ( -1.000000000000000000, 0.000000000000000000, 0.000000000000000000 ) ) ;
#24907=DIRECTION ( 'NONE',  ( 0.8660254037844378194, 0.5000000000000013323, 0.000000000000000000 ) ) ;
#25009=CARTESIAN_POINT ( 'NONE',  ( 0.000000000000000000, 0.000000000000000000, -8.949444346342716017 ) ) ;
#25053=B_SPLINE_CURVE_WITH_KNOTS ( 'NONE', 3,
 ( #21806, #11249, #43250, #54499, #4946, #21462, #54145, #42906 ),
 .UNSPECIFIED., .F., .F.,
 ( 4, 2, 2, 4 ),
 ( 0.004673709593152147908, 0.005837709341827640799, 0.007001709090503134558, 0.009329708587854120341 ),
 .UNSPECIFIED. ) ;
#25067=ORIENTED_EDGE ( 'NONE', *, *, #42256, .T. ) ;
#25250=DIRECTION ( 'NONE',  ( 0.000000000000000000, 0.000000000000000000, -1.000000000000000000 ) ) ;
#25514=CARTESIAN_POINT ( 'NONE',  ( 0.000000000000000000, 0.000000000000000000, -9.474599999999998801 ) ) ;
#25551=B_SPLINE_CURVE_WITH_KNOTS ( 'NONE', 3,
 ( #50777, #2598, #40568, #66984, #18776, #19113 ),
 .UNSPECIFIED., .F., .F.,
 ( 4, 2, 4 ),
 ( 2.380731629556566600E-07, 0.002336973833157566377, 0.004673709593152176531 ),
 .UNSPECIFIED. ) ;
#25593=VECTOR ( 'NONE', #49971, 1000.000000000000000 ) ;
#25790=DIRECTION ( 'NONE',  ( 0.000000000000000000, 0.000000000000000000, 1.000000000000000000 ) ) ;
#26006=DIRECTION ( 'NONE',  ( 0.000000000000000000, 0.000000000000000000, -1.000000000000000000 ) ) ;
#26118=CARTESIAN_POINT ( 'NONE',  ( 8.000000000000000000, 4.618802153516997855, -9.500000000000000000 ) ) ;
#26242=CIRCLE ( 'NONE', #59909, 8.000000000000000000 ) ;
#26441=ORIENTED_EDGE ( 'NONE', *, *, #7821, .T. ) ;
#26444=CARTESIAN_POINT ( 'NONE',  ( -2.644994884459114459, 7.710515798486365036, -9.417753204360289843 ) ) ;
#26508=CARTESIAN_POINT ( 'NONE',  ( -4.000000000000013323, 6.928203230275504332, -9.500000000000000000 ) ) ;
#26761=CONICAL_SURFACE ( 'NONE', #14418, 8.000000000000001776, 1.047197551196595855 ) ;
#26953=EDGE_LOOP ( 'NONE', ( #42216, #27102, #39010, #67899, #28667, #37534 ) ) ;
#26983=EDGE_CURVE ( 'NONE', #1313, #7482, #42095, .T. ) ;
#27031=ORIENTED_EDGE ( 'NONE', *, *, #62234, .T. ) ;
#27102=ORIENTED_EDGE ( 'NONE', *, *, #126, .F. ) ;
#27119=DIRECTION ( 'NONE',  ( -0.000000000000000000, -0.000000000000000000, 1.000000000000000000 ) ) ;
#27169=VECTOR ( 'NONE', #1695, 1000.000000000000000 ) ;
#27483=DIRECTION ( 'NONE',  ( -1.000000000000000000, 0.000000000000000000, 0.000000000000000000 ) ) ;
#27493=CARTESIAN_POINT ( 'NONE',  ( 8.000000000000001776, 0.000000000000000000, 0.000000000000000000 ) ) ;
#27497=PRODUCT_DEFINITION_CONTEXT ( 'detailed design', #37723, 'design' ) ;
#27627=CIRCLE ( 'NONE', #6289, 5.000000000000000888 ) ;
#27728=ORIENTED_EDGE ( 'NONE', *, *, #10618, .F. ) ;
#27749=CARTESIAN_POINT ( 'NONE',  ( -1.313474075707243838, -8.479269695850868871, -9.183279549040152645 ) ) ;
#27757=FILL_AREA_STYLE_COLOUR ( '', #35317 ) ;
#27772=DIRECTION ( 'NONE',  ( 0.000000000000000000, -0.000000000000000000, 1.000000000000000000 ) ) ;
#27849=CARTESIAN_POINT ( 'NONE',  ( 0.000000000000000000, 0.000000000000000000, 3.469446951953614189E-15 ) ) ;
#27867=AXIS2_PLACEMENT_3D ( 'NONE', #2283, #45876, #67690 ) ;
#27904=EDGE_LOOP ( 'NONE', ( #13589, #45281, #6791, #68277, #16195, #10976 ) ) ;
#28235=DIRECTION ( 'NONE',  ( -1.000000000000000000, 0.000000000000000000, 0.000000000000000000 ) ) ;
#28295=AXIS2_PLACEMENT_3D ( 'NONE', #53054, #26006, #31285 ) ;
#28415=ORIENTED_EDGE ( 'NONE', *, *, #58194, .F. ) ;
#28667=ORIENTED_EDGE ( 'NONE', *, *, #38257, .T. ) ;
#28779=EDGE_CURVE ( 'NONE', #66775, #36668, #32197, .T. ) ;
#29071=ORIENTED_EDGE ( 'NONE', *, *, #37207, .F. ) ;
#29081=PLANE ( 'NONE',  #65213 ) ;
#29114=EDGE_LOOP ( 'NONE', ( #24605, #20671, #33954, #64458 ) ) ;
#29309=VERTEX_POINT ( 'NONE', #11848 ) ;
#29380=ORIENTED_EDGE ( 'NONE', *, *, #47710, .T. ) ;
#29412=CARTESIAN_POINT ( 'NONE',  ( -8.000000000000000000, 0.7809653281576073303, -9.500000000000001776 ) ) ;
#29526=CARTESIAN_POINT ( 'NONE',  ( 8.000000000000000000, -4.618802153517021836, -9.500000000000000000 ) ) ;
#29557=EDGE_CURVE ( 'NONE', #52636, #36166, #5276, .T. ) ;
#29559=CARTESIAN_POINT ( 'NONE',  ( 0.6527133886630186455, -8.860760056385776906, -0.4969600502617733118 ) ) ;
#29601=DIRECTION ( 'NONE',  ( -0.000000000000000000, -0.000000000000000000, 1.000000000000000000 ) ) ;
#29610=CARTESIAN_POINT ( 'NONE',  ( -4.000000000000009770, -6.928203230275505220, -9.500000000000000000 ) ) ;
#29621=ORIENTED_EDGE ( 'NONE', *, *, #54069, .F. ) ;
#29724=FACE_OUTER_BOUND ( 'NONE', #15606, .T. ) ;
#29747=DIRECTION ( 'NONE',  ( -0.5000000000000014433, 0.8660254037844378194, 0.000000000000000000 ) ) ;
#29751=VERTEX_POINT ( 'NONE', #67169 ) ;
#30132=ORIENTED_EDGE ( 'NONE', *, *, #61711, .F. ) ;
#30158=ORIENTED_EDGE ( 'NONE', *, *, #30733, .T. ) ;
#30178=LINE ( 'NONE', #7067, #25593 ) ;
#30231=CARTESIAN_POINT ( 'NONE',  ( 8.000000000000000000, 4.618802153516997855, -9.500000000000000000 ) ) ;
#30511=B_SPLINE_CURVE_WITH_KNOTS ( 'NONE', 3,
 ( #39788, #50683, #49629, #45764, #17992, #23276 ),
 .UNSPECIFIED., .F., .F.,
 ( 4, 2, 4 ),
 ( 2.380731629548242913E-07, 0.002336973833157547729, 0.004673709593152140102 ),
 .UNSPECIFIED. ) ;
#30590=ADVANCED_FACE ( 'NONE', ( #44659 ), #44288, .F. ) ;
#30733=EDGE_CURVE ( 'NONE', #56693, #49487, #41342, .T. ) ;
#30789=CARTESIAN_POINT ( 'NONE',  ( 8.000000000000000000, 3.871967595402134421, -9.001061386767540640 ) ) ;
#30792=DIRECTION ( 'NONE',  ( -0.8660254037844378194, -0.5000000000000014433, 0.000000000000000000 ) ) ;
#30794=ORIENTED_EDGE ( 'NONE', *, *, #29557, .T. ) ;
#30901=AXIS2_PLACEMENT_3D ( 'NONE', #25514, #15291, #19880 ) ;
#30982=CARTESIAN_POINT ( 'NONE',  ( -8.000000000000000000, -3.867591403079184253, -0.4976753153245863648 ) ) ;
#31067=EDGE_CURVE ( 'NONE', #1172, #15636, #66745, .T. ) ;
#31187=VERTEX_POINT ( 'NONE', #21977 ) ;
#31191=CARTESIAN_POINT ( 'NONE',  ( 0.000000000000000000, 0.000000000000000000, -9.474599999999998801 ) ) ;
#31196=ORIENTED_EDGE ( 'NONE', *, *, #22396, .T. ) ;
#31252=CIRCLE ( 'NONE', #49178, 5.000000000000000888 ) ;
#31285=DIRECTION ( 'NONE',  ( -1.000000000000000000, 0.000000000000000000, 0.000000000000000000 ) ) ;
#31397=ADVANCED_FACE ( 'NONE', ( #13860 ), #61619, .F. ) ;
#31485=B_SPLINE_CURVE_WITH_KNOTS ( 'NONE', 3,
 ( #1489, #7116, #7481, #55294, #17675, #23309 ),
 .UNSPECIFIED., .F., .F.,
 ( 4, 2, 4 ),
 ( 2.380731629582122378E-07, 0.002336973833157553367, 0.004673709593152147908 ),
 .UNSPECIFIED. ) ;
#31503=SHAPE_DEFINITION_REPRESENTATION ( #64137, #50551 ) ;
#31584=CARTESIAN_POINT ( 'NONE',  ( 8.000000000000001776, 0.000000000000000000, -9.500000000000000000 ) ) ;
#31627=VERTEX_POINT ( 'NONE', #59776 ) ;
#31657=CARTESIAN_POINT ( 'NONE',  ( -8.000000000000000000, -3.098204225878178342, -0.3157906771918749800 ) ) ;
#31683=EDGE_CURVE ( 'NONE', #59496, #29751, #36679, .T. ) ;
#31712=CARTESIAN_POINT ( 'NONE',  ( -1.310872448937997703, 8.480771745766402248, -9.182649155111340278 ) ) ;
#31802=DIRECTION ( 'NONE',  ( -0.000000000000000000, -0.000000000000000000, 1.000000000000000000 ) ) ;
#31841=CARTESIAN_POINT ( 'NONE',  ( 0.000000000000000000, 0.000000000000000000, -8.949444346342716017 ) ) ;
#31882=EDGE_LOOP ( 'NONE', ( #30794, #34826, #14598, #35412 ) ) ;
#31993=ORIENTED_EDGE ( 'NONE', *, *, #20414, .F. ) ;
#32006=ORIENTED_EDGE ( 'NONE', *, *, #26983, .F. ) ;
#32114=FACE_BOUND ( 'NONE', #40147, .T. ) ;
#32197=CIRCLE ( 'NONE', #34425, 4.999999999999999112 ) ;
#32254=CONICAL_SURFACE ( 'NONE', #9817, 4.174999999999999822, 0.9599310885968758145 ) ;
#32345=AXIS2_PLACEMENT_3D ( 'NONE', #9106, #23897, #7724 ) ;
#32476=CARTESIAN_POINT ( 'NONE',  ( 8.000000000000000000, 4.618802153517024500, -8.785468820183664818 ) ) ;
#32493=CARTESIAN_POINT ( 'NONE',  ( 0.000000000000000000, 0.000000000000000000, -25.03750572909317285 ) ) ;
#32590=AXIS2_PLACEMENT_3D ( 'NONE', #31191, #19940, #35421 ) ;
#32637=ORIENTED_EDGE ( 'NONE', *, *, #21731, .F. ) ;
#32667=AXIS2_PLACEMENT_3D ( 'NONE', #3778, #25250, #45659 ) ;
#32753=CARTESIAN_POINT ( 'NONE',  ( 0.000000000000000000, 0.000000000000000000, 0.000000000000000000 ) ) ;
#33042=CARTESIAN_POINT ( 'NONE',  ( 2.644994884459111795, -7.710515798486388128, -9.417753204360273855 ) ) ;
#33043=PRESENTATION_STYLE_ASSIGNMENT (( #5007 ) ) ;
#33230=CARTESIAN_POINT ( 'NONE',  ( -8.000000000000000000, -3.098204225878183671, -9.184209322808126075 ) ) ;
#33312=CARTESIAN_POINT ( 'NONE',  ( -4.250000000000000000, 5.204748896376250699E-16, -9.500000000000000000 ) ) ;
#33398=CARTESIAN_POINT ( 'NONE',  ( -3.318518101603030068, -7.321656987762886537, -9.499999999999994671 ) ) ;
#33538=CARTESIAN_POINT ( 'NONE',  ( 4.339467034331195627, 6.732211846623388674, -9.500000000000003553 ) ) ;
#33583=ORIENTED_EDGE ( 'NONE', *, *, #53481, .F. ) ;
#33757=VERTEX_POINT ( 'NONE', #47184 ) ;
#33954=ORIENTED_EDGE ( 'NONE', *, *, #11242, .T. ) ;
#34204=CARTESIAN_POINT ( 'NONE',  ( 0.000000000000000000, 0.000000000000000000, -9.500000000000000000 ) ) ;
#34251=DIRECTION ( 'NONE',  ( -1.000000000000000000, -1.776356839400250465E-15, 0.000000000000000000 ) ) ;
#34273=ORIENTED_EDGE ( 'NONE', *, *, #46385, .F. ) ;
#34299=B_SPLINE_CURVE_WITH_KNOTS ( 'NONE', 3,
 ( #66634, #6488, #33230, #60646, #12818, #34630 ),
 .UNSPECIFIED., .F., .F.,
 ( 4, 2, 4 ),
 ( 0.008240550023493531037, 0.01057684187039406240, 0.01291313371729459550 ),
 .UNSPECIFIED. ) ;
#34416=B_SPLINE_CURVE_WITH_KNOTS ( 'NONE', 3,
 ( #55024, #37454, #5453, #11769, #17393, #43421 ),
 .UNSPECIFIED., .F., .F.,
 ( 4, 2, 4 ),
 ( 0.01291313371729459203, 0.01525081363757309870, 0.01758849355785160537 ),
 .UNSPECIFIED. ) ;
#34425=AXIS2_PLACEMENT_3D ( 'NONE', #27849, #49286, #7091 ) ;
#34630=CARTESIAN_POINT ( 'NONE',  ( -8.000000000000000000, 0.000000000000000000, -9.500000000000000000 ) ) ;
#34657=DIRECTION ( 'NONE',  ( 1.000000000000000000, 0.000000000000000000, 0.000000000000000000 ) ) ;
#34693=DIRECTION ( 'NONE',  ( -1.000000000000000000, 0.000000000000000000, 0.000000000000000000 ) ) ;
#34699=ORIENTED_EDGE ( 'NONE', *, *, #48332, .F. ) ;
#34826=ORIENTED_EDGE ( 'NONE', *, *, #9536, .T. ) ;
#34838=FACE_OUTER_BOUND ( 'NONE', #49341, .T. ) ;
#34984=CARTESIAN_POINT ( 'NONE',  ( -7.347286611336974360, -4.995646404165295706, -0.4969600502617599891 ) ) ;
#35046=DIRECTION ( 'NONE',  ( -0.8191520442889886899, 1.003171929053520926E-16, 0.5735764363510506003 ) ) ;
#35317=COLOUR_RGB ( '',0.7921568627450980005, 0.8196078431372548767, 0.9333333333333333481 ) ;
#35330=ORIENTED_EDGE ( 'NONE', *, *, #6105, .F. ) ;
#35357=EDGE_CURVE ( 'NONE', #29309, #17325, #64088, .T. ) ;
#35412=ORIENTED_EDGE ( 'NONE', *, *, #11242, .F. ) ;
#35421=DIRECTION ( 'NONE',  ( -1.000000000000000000, 0.000000000000000000, 0.000000000000000000 ) ) ;
#35430=ORIENTED_EDGE ( 'NONE', *, *, #11600, .F. ) ;
#35464=DIRECTION ( 'NONE',  ( 0.000000000000000000, 0.000000000000000000, 1.000000000000000000 ) ) ;
#35538=ORIENTED_EDGE ( 'NONE', *, *, #40705, .F. ) ;
#35556=DIRECTION ( 'NONE',  ( -1.000000000000000000, 0.000000000000000000, 0.000000000000000000 ) ) ;
#35604=EDGE_CURVE ( 'NONE', #20984, #902, #21398, .T. ) ;
#35661=CARTESIAN_POINT ( 'NONE',  ( 8.000000000000000000, 4.618802153516997855, -9.500000000000000000 ) ) ;
#36025=DIRECTION ( 'NONE',  ( 0.000000000000000000, -0.000000000000000000, 1.000000000000000000 ) ) ;
#36067=PLANE ( 'NONE',  #11219 ) ;
#36088=CARTESIAN_POINT ( 'NONE',  ( 5.690023276062394331, 5.952467836904148157, -0.1306530452038075496 ) ) ;
#36166=VERTEX_POINT ( 'NONE', #8216 ) ;
#36197=DIRECTION ( 'NONE',  ( 0.8191520442889886899, 0.000000000000000000, 0.5735764363510506003 ) ) ;
#36230=VECTOR ( 'NONE', #53915, 1000.000000000000000 ) ;
#36326=PLANE ( 'NONE',  #67064 ) ;
#36329=AXIS2_PLACEMENT_3D ( 'NONE', #51308, #35464, #42119 ) ;
#36347=FACE_OUTER_BOUND ( 'NONE', #27904, .T. ) ;
#36354=FACE_OUTER_BOUND ( 'NONE', #59896, .T. ) ;
#36433=CONICAL_SURFACE ( 'NONE', #46511, 8.000000000000001776, 1.047197551196595855 ) ;
#36492=PLANE ( 'NONE',  #55007 ) ;
#36668=VERTEX_POINT ( 'NONE', #65867 ) ;
#36679=B_SPLINE_CURVE_WITH_KNOTS ( 'NONE', 3,
 ( #55208, #50293, #7027, #1400, #11588, #11953 ),
 .UNSPECIFIED., .F., .F.,
 ( 4, 2, 4 ),
 ( 0.01291313371729459203, 0.01525081363757311431, 0.01758849355785163660 ),
 .UNSPECIFIED. ) ;
#36792=FACE_OUTER_BOUND ( 'NONE', #49623, .T. ) ;
#36822=LINE ( 'NONE', #14665, #36230 ) ;
#36993=CARTESIAN_POINT ( 'NONE',  ( -2.309976723937614107, 7.903938623646865835, -9.369346954796188953 ) ) ;
#37120=AXIS2_PLACEMENT_3D ( 'NONE', #61823, #8733, #24906 ) ;
#37126=ORIENTED_EDGE ( 'NONE', *, *, #17240, .F. ) ;
#37207=EDGE_CURVE ( 'NONE', #17325, #21790, #34416, .T. ) ;
#37287=ORIENTED_EDGE ( 'NONE', *, *, #8979, .F. ) ;
#37288=ORIENTED_EDGE ( 'NONE', *, *, #62884, .T. ) ;
#37371=DIRECTION ( 'NONE',  ( -1.000000000000000000, 0.000000000000000000, 0.000000000000000000 ) ) ;
#37398=DIRECTION ( 'NONE',  ( 0.000000000000000000, -0.000000000000000000, 1.000000000000000000 ) ) ;
#37412=FACE_OUTER_BOUND ( 'NONE', #48634, .T. ) ;
#37454=CARTESIAN_POINT ( 'NONE',  ( -8.000000000000000000, 0.7809653281576027783, 9.834052517622422992E-16 ) ) ;
#37534=ORIENTED_EDGE ( 'NONE', *, *, #31683, .F. ) ;
#37699=ADVANCED_FACE ( 'NONE', ( #39817 ), #51884, .T. ) ;
#37723=APPLICATION_CONTEXT ( 'automotive_design' ) ;
#37776=CARTESIAN_POINT ( 'NONE',  ( -8.000000000000000000, -4.618802153517024500, -8.785468820183664818 ) ) ;
#37865=CONICAL_SURFACE ( 'NONE', #9815, 8.000000000000001776, 1.047197551196595855 ) ;
#37957=VECTOR ( 'NONE', #8686, 1000.000000000000000 ) ;
#38244=EDGE_LOOP ( 'NONE', ( #45118, #32637, #16207 ) ) ;
#38257=EDGE_CURVE ( 'NONE', #61707, #29751, #7031, .T. ) ;
#38319=DIRECTION ( 'NONE',  ( 0.000000000000000000, 0.000000000000000000, 1.000000000000000000 ) ) ;
#38396=DIRECTION ( 'NONE',  ( -0.000000000000000000, -0.000000000000000000, 1.000000000000000000 ) ) ;
#38423=VECTOR ( 'NONE', #51680, 1000.000000000000000 ) ;
#38580=DIRECTION ( 'NONE',  ( -0.000000000000000000, 0.000000000000000000, -1.000000000000000000 ) ) ;
#38599=EDGE_LOOP ( 'NONE', ( #13458, #37287, #24657, #985 ) ) ;
#38613=DIRECTION ( 'NONE',  ( 1.000000000000000000, 0.000000000000000000, 0.000000000000000000 ) ) ;
#38757=B_SPLINE_CURVE_WITH_KNOTS ( 'NONE', 3,
 ( #55088, #29412, #2679, #60721, #49455, #11835 ),
 .UNSPECIFIED., .F., .F.,
 ( 4, 2, 4 ),
 ( 0.01291313371729459550, 0.01525081363757311778, 0.01758849355785164006 ),
 .UNSPECIFIED. ) ;
#38848=DIRECTION ( 'NONE',  ( -1.000000000000000000, 3.552713678800500929E-15, 0.000000000000000000 ) ) ;
#38945=VERTEX_POINT ( 'NONE', #15523 ) ;
#38953=CONICAL_SURFACE ( 'NONE', #56925, 8.000000000000001776, 1.047197551196595855 ) ;
#39000=CARTESIAN_POINT ( 'NONE',  ( -4.250000000000000000, 5.204748896376250699E-16, -0.5251556536572842271 ) ) ;
#39010=ORIENTED_EDGE ( 'NONE', *, *, #54069, .T. ) ;
#39027=CARTESIAN_POINT ( 'NONE',  ( -3.816391647148975608E-14, -9.237604307034022355, -8.785468820183664818 ) ) ;
#39120=CARTESIAN_POINT ( 'NONE',  ( -1.734723475976807094E-15, 9.237604307034022355, -8.785468820183664818 ) ) ;
#39183=VERTEX_POINT ( 'NONE', #42780 ) ;
#39187=CARTESIAN_POINT ( 'NONE',  ( 4.000000000000012434, 6.928203230275504332, -9.500000000000000000 ) ) ;
#39420=CARTESIAN_POINT ( 'NONE',  ( -3.816391647148975608E-14, -9.237604307034022355, -0.7145311798163346273 ) ) ;
#39494=CARTESIAN_POINT ( 'NONE',  ( 6.689127551062003185, 5.375634714784618851, -9.182649155111345607 ) ) ;
#39770=CARTESIAN_POINT ( 'NONE',  ( 4.000000000000011546, -6.928203230275505220, 0.000000000000000000 ) ) ;
#39788=CARTESIAN_POINT ( 'NONE',  ( 8.000000000000003553, -4.618802153517020948, -8.785468820183664818 ) ) ;
#39817=FACE_OUTER_BOUND ( 'NONE', #18634, .T. ) ;
#40031=ORIENTED_EDGE ( 'NONE', *, *, #63782, .T. ) ;
#40095=DIRECTION ( 'NONE',  ( 0.000000000000000000, 0.000000000000000000, 1.000000000000000000 ) ) ;
#40147=EDGE_LOOP ( 'NONE', ( #58011, #43051 ) ) ;
#40348=FACE_OUTER_BOUND ( 'NONE', #29114, .T. ) ;
#40545=AXIS2_PLACEMENT_3D ( 'NONE', #16804, #66075, #23498 ) ;
#40568=CARTESIAN_POINT ( 'NONE',  ( 1.313474075707213196, 8.479269695850863542, -0.3167204509598407491 ) ) ;
#40596=CARTESIAN_POINT ( 'NONE',  ( -8.000000000000000000, -4.618802153517024500, -0.7145311798163346273 ) ) ;
#40597=ORIENTED_EDGE ( 'NONE', *, *, #19719, .F. ) ;
#40705=EDGE_CURVE ( 'NONE', #902, #20984, #43012, .T. ) ;
#40780=AXIS2_PLACEMENT_3D ( 'NONE', #57790, #3294, #62379 ) ;
#40824=MANIFOLD_SOLID_BREP ( 'EndChamfer', #61987 ) ;
#41064=CARTESIAN_POINT ( 'NONE',  ( 0.000000000000000000, 0.000000000000000000, 0.000000000000000000 ) ) ;
#41278=( LENGTH_UNIT ( ) NAMED_UNIT ( * ) SI_UNIT ( .MILLI., .METRE. ) );
#41279=CONICAL_SURFACE ( 'NONE', #68250, 8.000000000000001776, 1.047197551196595855 ) ;
#41342=CIRCLE ( 'NONE', #32345, 5.000000000000000888 ) ;
#41349=FACE_OUTER_BOUND ( 'NONE', #16769, .T. ) ;
#41460=ADVANCED_FACE ( 'NONE', ( #36347 ), #24762, .T. ) ;
#41612=UNCERTAINTY_MEASURE_WITH_UNIT (LENGTH_MEASURE( 1.000000000000000082E-05 ), #41278, 'distance_accuracy_value', 'NONE');
#41651=CARTESIAN_POINT ( 'NONE',  ( -0.6543471694412734685, -8.859816792613656844, -0.4964154566688013248 ) ) ;
#41661=DIRECTION ( 'NONE',  ( -1.000000000000000000, 0.000000000000000000, 0.000000000000000000 ) ) ;
#41748=AXIS2_PLACEMENT_3D ( 'NONE', #34204, #29601, #24347 ) ;
#41761=ORIENTED_EDGE ( 'NONE', *, *, #8511, .T. ) ;
#41825=ORIENTED_EDGE ( 'NONE', *, *, #43355, .T. ) ;
#41866=DIRECTION ( 'NONE',  ( 1.000000000000000000, 0.000000000000000000, 0.000000000000000000 ) ) ;
#41919=DIRECTION ( 'NONE',  ( -0.000000000000000000, 0.000000000000000000, -1.000000000000000000 ) ) ;
#42095=B_SPLINE_CURVE_WITH_KNOTS ( 'NONE', 3,
 ( #39770, #44703, #2489, #23943, #19009, #46081, #29559, #39420 ),
 .UNSPECIFIED., .F., .F.,
 ( 4, 2, 2, 4 ),
 ( 0.004673709593152140102, 0.005837709341827639065, 0.007001709090503138895, 0.009329708587854137689 ),
 .UNSPECIFIED. ) ;
#42119=DIRECTION ( 'NONE',  ( 1.000000000000000000, 0.000000000000000000, 0.000000000000000000 ) ) ;
#42216=ORIENTED_EDGE ( 'NONE', *, *, #62641, .F. ) ;
#42256=EDGE_CURVE ( 'NONE', #57574, #1313, #7167, .T. ) ;
#42338=DIRECTION ( 'NONE',  ( -1.000000000000000000, 0.000000000000000000, 0.000000000000000000 ) ) ;
#42339=DIRECTION ( 'NONE',  ( -0.000000000000000000, -0.000000000000000000, 1.000000000000000000 ) ) ;
#42780=CARTESIAN_POINT ( 'NONE',  ( 4.000000000000012434, 6.928203230275504332, 0.000000000000000000 ) ) ;
#42836=VERTEX_POINT ( 'NONE', #48202 ) ;
#42906=CARTESIAN_POINT ( 'NONE',  ( -1.734723475976807094E-15, 9.237604307034022355, -0.7145311798163346273 ) ) ;
#42990=DIRECTION ( 'NONE',  ( -1.000000000000000000, 0.000000000000000000, 0.000000000000000000 ) ) ;
#43012=CIRCLE ( 'NONE', #40780, 4.250000000000000000 ) ;
#43051=ORIENTED_EDGE ( 'NONE', *, *, #28779, .F. ) ;
#43070=AXIS2_PLACEMENT_3D ( 'NONE', #35661, #52518, #62389 ) ;
#43104=CARTESIAN_POINT ( 'NONE',  ( 8.000000000000000000, -3.867591403079183365, -0.4976753153245864758 ) ) ;
#43111=ORIENTED_EDGE ( 'NONE', *, *, #40705, .T. ) ;
#43250=CARTESIAN_POINT ( 'NONE',  ( -3.319543390096042490, 7.321065037175422674, -0.01688885742776483068 ) ) ;
#43265=CARTESIAN_POINT ( 'NONE',  ( 8.000000000000003553, -4.618802153517020948, -0.7145311798163346273 ) ) ;
#43313=ORIENTED_EDGE ( 'NONE', *, *, #17240, .T. ) ;
#43355=EDGE_CURVE ( 'NONE', #989, #58090, #20742, .T. ) ;
#43421=CARTESIAN_POINT ( 'NONE',  ( -8.000000000000000000, 4.618802153516996079, -0.7145311798163263006 ) ) ;
#43540=LINE ( 'NONE', #21742, #27169 ) ;
#43595=DIRECTION ( 'NONE',  ( 1.000000000000000000, 0.000000000000000000, 0.000000000000000000 ) ) ;
#43611=CARTESIAN_POINT ( 'NONE',  ( 0.000000000000000000, 0.000000000000000000, 0.000000000000000000 ) ) ;
#43729=CARTESIAN_POINT ( 'NONE',  ( 4.000000000000011546, -6.928203230275505220, 0.000000000000000000 ) ) ;
#43791=CARTESIAN_POINT ( 'NONE',  ( 8.000000000000000000, -3.098204225878178342, -0.3157906771918749245 ) ) ;
#43870=DIRECTION ( 'NONE',  ( -0.000000000000000000, -0.000000000000000000, 1.000000000000000000 ) ) ;
#43886=DIRECTION ( 'NONE',  ( 0.8191520442889916875, 1.003171929053524623E-16, -0.5735764363510462704 ) ) ;
#43965=ORIENTED_EDGE ( 'NONE', *, *, #4998, .T. ) ;
#43987=AXIS2_PLACEMENT_3D ( 'NONE', #4273, #58409, #53123 ) ;
#44057=CARTESIAN_POINT ( 'NONE',  ( 4.000000000000012434, 6.928203230275504332, -9.500000000000000000 ) ) ;
#44072=CARTESIAN_POINT ( 'NONE',  ( -4.000000000000013323, 6.928203230275504332, 0.000000000000000000 ) ) ;
#44085=CARTESIAN_POINT ( 'NONE',  ( 1.313474075707213196, 8.479269695850863542, -9.183279549040157974 ) ) ;
#44288=CYLINDRICAL_SURFACE ( 'NONE', #811, 4.250000000000000000 ) ;
#44309=DIRECTION ( 'NONE',  ( 0.000000000000000000, 0.000000000000000000, 1.000000000000000000 ) ) ;
#44487=VERTEX_POINT ( 'NONE', #12171 ) ;
#44558=DIRECTION ( 'NONE',  ( 0.000000000000000000, 0.000000000000000000, 1.000000000000000000 ) ) ;
#44659=FACE_OUTER_BOUND ( 'NONE', #38599, .T. ) ;
#44703=CARTESIAN_POINT ( 'NONE',  ( 3.660532965668830130, -7.124194613927636865, -5.418258005348944116E-15 ) ) ;
#44750=EDGE_LOOP ( 'NONE', ( #68121, #25067, #66950, #66747, #59828, #35430 ) ) ;
#44807=CARTESIAN_POINT ( 'NONE',  ( 0.6543471694412384965, 8.859816792613651515, -9.003584543331202283 ) ) ;
#44871=B_SPLINE_CURVE_WITH_KNOTS ( 'NONE', 3,
 ( #45530, #24441, #45881, #18802, #19841, #13531, #34984, #40596 ),
 .UNSPECIFIED., .F., .F.,
 ( 4, 2, 2, 4 ),
 ( 0.004673709593152186939, 0.005837709341827670290, 0.007001709090503154508, 0.009329708587854118607 ),
 .UNSPECIFIED. ) ;
#45082=VERTEX_POINT ( 'NONE', #44072 ) ;
#45092=CARTESIAN_POINT ( 'NONE',  ( -4.339467034331206285, -6.732211846623409102, -9.499999999999992895 ) ) ;
#45118=ORIENTED_EDGE ( 'NONE', *, *, #56861, .T. ) ;
#45281=ORIENTED_EDGE ( 'NONE', *, *, #12373, .T. ) ;
#45365=LINE ( 'NONE', #29526, #20415 ) ;
#45530=CARTESIAN_POINT ( 'NONE',  ( -4.000000000000009770, -6.928203230275505220, 0.000000000000000000 ) ) ;
#45659=DIRECTION ( 'NONE',  ( -1.000000000000000000, 0.000000000000000000, 0.000000000000000000 ) ) ;
#45669=ORIENTED_EDGE ( 'NONE', *, *, #62234, .F. ) ;
#45677=LINE ( 'NONE', #1721, #14978 ) ;
#45695=ORIENTED_EDGE ( 'NONE', *, *, #9206, .F. ) ;
#45711=AXIS2_PLACEMENT_3D ( 'NONE', #31841, #20587, #15322 ) ;
#45758=APPLICATION_CONTEXT ( 'automotive_design' ) ;
#45764=CARTESIAN_POINT ( 'NONE',  ( 5.354491962338135735, -6.146186931204420389, -9.431901280394560771 ) ) ;
#45767=DIRECTION ( 'NONE',  ( -0.000000000000000000, -0.000000000000000000, 1.000000000000000000 ) ) ;
#45805=EDGE_LOOP ( 'NONE', ( #27728, #7225, #11693 ) ) ;
#45876=DIRECTION ( 'NONE',  ( 0.000000000000000000, 0.000000000000000000, -1.000000000000000000 ) ) ;
#45881=CARTESIAN_POINT ( 'NONE',  ( -4.680456609903986376, -6.535341423375604641, -0.01688885742777731375 ) ) ;
#45885=DIRECTION ( 'NONE',  ( -0.000000000000000000, -0.000000000000000000, 1.000000000000000000 ) ) ;
#45980=EDGE_LOOP ( 'NONE', ( #11851, #11817, #10139 ) ) ;
#46081=CARTESIAN_POINT ( 'NONE',  ( 1.310872448937990153, -8.480771745766427117, -0.3173508448886726563 ) ) ;
#46217=CIRCLE ( 'NONE', #15887, 8.000000000000000000 ) ;
#46337=ADVANCED_FACE ( 'NONE', ( #14861 ), #36326, .T. ) ;
#46385=EDGE_CURVE ( 'NONE', #21805, #31627, #11951, .T. ) ;
#46511=AXIS2_PLACEMENT_3D ( 'NONE', #56791, #45885, #34657 ) ;
#46802=CARTESIAN_POINT ( 'NONE',  ( -8.000000000000001776, 0.000000000000000000, 0.000000000000000000 ) ) ;
#46833=EDGE_CURVE ( 'NONE', #49487, #58090, #49899, .T. ) ;
#46846=VECTOR ( 'NONE', #12277, 1000.000000000000000 ) ;
#46921=FACE_OUTER_BOUND ( 'NONE', #38244, .T. ) ;
#47041=CARTESIAN_POINT ( 'NONE',  ( 5.007715329123879543E-16, -9.237604307034043671, -9.500000000000000000 ) ) ;
#47184=CARTESIAN_POINT ( 'NONE',  ( 8.000000000000001776, 0.000000000000000000, -9.500000000000000000 ) ) ;
#47254=CARTESIAN_POINT ( 'NONE',  ( 0.000000000000000000, 0.000000000000000000, -9.500000000000000000 ) ) ;
#47308=CARTESIAN_POINT ( 'NONE',  ( 5.355005115540897975, 6.145890662064649845, -0.08224679563971175333 ) ) ;
#47318=VERTEX_POINT ( 'NONE', #39120 ) ;
#47488=STYLED_ITEM ( 'NONE', ( #33043 ), #40824 ) ;
#47556=VECTOR ( 'NONE', #44309, 1000.000000000000000 ) ;
#47710=EDGE_CURVE ( 'NONE', #20984, #66775, #24834, .T. ) ;
#47827=CARTESIAN_POINT ( 'NONE',  ( -8.000000000000000000, -1.555946510856143883, -0.06708870216335346970 ) ) ;
#47876=DIRECTION ( 'NONE',  ( -1.000000000000000000, 0.000000000000000000, 0.000000000000000000 ) ) ;
#47881=CARTESIAN_POINT ( 'NONE',  ( -1.734723475976807094E-15, 9.237604307034022355, -8.785468820183664818 ) ) ;
#48180=CARTESIAN_POINT ( 'NONE',  ( 0.000000000000000000, 0.000000000000000000, -9.500000000000000000 ) ) ;
#48202=CARTESIAN_POINT ( 'NONE',  ( 8.000000000000003553, -4.618802153517020948, -8.785468820183664818 ) ) ;
#48332=EDGE_CURVE ( 'NONE', #49487, #56693, #31252, .T. ) ;
#48518=FACE_OUTER_BOUND ( 'NONE', #9887, .T. ) ;
#48601=CIRCLE ( 'NONE', #14941, 8.000000000000000000 ) ;
#48634=EDGE_LOOP ( 'NONE', ( #34699, #52794, #26441, #3279 ) ) ;
#48712=CARTESIAN_POINT ( 'NONE',  ( 8.000000000000000000, -1.555946510856143661, -0.06708870216335349745 ) ) ;
#49051=VECTOR ( 'NONE', #43886, 1000.000000000000000 ) ;
#49115=ADVANCED_FACE ( 'NONE', ( #64115 ), #26761, .T. ) ;
#49175=ADVANCED_BREP_SHAPE_REPRESENTATION ( '', ( #40824, #66832 ), #3998 ) ;
#49178=AXIS2_PLACEMENT_3D ( 'NONE', #58391, #27772, #64717 ) ;
#49225=DIRECTION ( 'NONE',  ( -0.000000000000000000, -0.000000000000000000, 1.000000000000000000 ) ) ;
#49277=CARTESIAN_POINT ( 'NONE',  ( 0.000000000000000000, 0.000000000000000000, -9.500000000000000000 ) ) ;
#49286=DIRECTION ( 'NONE',  ( -0.000000000000000000, -0.000000000000000000, 1.000000000000000000 ) ) ;
#49290=B_SPLINE_CURVE_WITH_KNOTS ( 'NONE', 3,
 ( #9174, #30982, #31657, #47827, #14788, #46802 ),
 .UNSPECIFIED., .F., .F.,
 ( 4, 2, 4 ),
 ( 0.008240550023493531037, 0.01057684187039406240, 0.01291313371729459203 ),
 .UNSPECIFIED. ) ;
#49341=EDGE_LOOP ( 'NONE', ( #34273, #4013, #37126, #35330, #67844, #45669 ) ) ;
#49437=CARTESIAN_POINT ( 'NONE',  ( 4.250000000000000000, 0.000000000000000000, -0.5251556536572842271 ) ) ;
#49455=CARTESIAN_POINT ( 'NONE',  ( -8.000000000000000000, 3.871967595402135753, -9.001061386767540640 ) ) ;
#49487=VERTEX_POINT ( 'NONE', #60140 ) ;
#49517=B_SPLINE_CURVE_WITH_KNOTS ( 'NONE', 3,
 ( #64635, #21369, #5538, #22067, #53366, #31584 ),
 .UNSPECIFIED., .F., .F.,
 ( 4, 2, 4 ),
 ( 0.008240550023493532772, 0.01057684187039406240, 0.01291313371729459550 ),
 .UNSPECIFIED. ) ;
#49533=ADVANCED_FACE ( 'NONE', ( #48518 ), #41279, .T. ) ;
#49564=EDGE_CURVE ( 'NONE', #45082, #38945, #25053, .T. ) ;
#49623=EDGE_LOOP ( 'NONE', ( #21180, #54997, #8043 ) ) ;
#49629=CARTESIAN_POINT ( 'NONE',  ( 6.686525924292799239, -5.377136764700172655, -9.183279549040156198 ) ) ;
#49660=CARTESIAN_POINT ( 'NONE',  ( 8.000000000000000000, 4.618802153517024500, -8.785468820183664818 ) ) ;
#49899=LINE ( 'NONE', #8040, #46846 ) ;
#49906=CARTESIAN_POINT ( 'NONE',  ( 3.319543390096042934, -7.321065037175443990, -9.483111142572223429 ) ) ;
#49931=ORIENTED_EDGE ( 'NONE', *, *, #59760, .T. ) ;
#49971=DIRECTION ( 'NONE',  ( -0.000000000000000000, -0.000000000000000000, 1.000000000000000000 ) ) ;
#50229=AXIS2_PLACEMENT_3D ( 'NONE', #47254, #36025, #20879 ) ;
#50293=CARTESIAN_POINT ( 'NONE',  ( 8.000000000000000000, 0.7809653281576085515, 9.452887691357987840E-16 ) ) ;
#50299=DIRECTION ( 'NONE',  ( -1.000000000000000000, 0.000000000000000000, 0.000000000000000000 ) ) ;
#50507=CARTESIAN_POINT ( 'NONE',  ( -5.000000000000000888, 0.000000000000000000, -9.474599999999998801 ) ) ;
#50530=CARTESIAN_POINT ( 'NONE',  ( 0.000000000000000000, 0.000000000000000000, 0.000000000000000000 ) ) ;
#50551=SHAPE_REPRESENTATION ( 'hex nut gradec_iso_ISO - 4034 - M10 - N', ( #66832 ), #3998 ) ;
#50575=EDGE_CURVE ( 'NONE', #36668, #66775, #65251, .T. ) ;
#50618=ORIENTED_EDGE ( 'NONE', *, *, #58194, .T. ) ;
#50665=ORIENTED_EDGE ( 'NONE', *, *, #55163, .T. ) ;
#50683=CARTESIAN_POINT ( 'NONE',  ( 7.345652830558766055, -4.996589667937388235, -9.003584543331200507 ) ) ;
#50719=DIRECTION ( 'NONE',  ( 0.000000000000000000, 0.000000000000000000, -1.000000000000000000 ) ) ;
#50777=CARTESIAN_POINT ( 'NONE',  ( -1.734723475976807094E-15, 9.237604307034022355, -0.7145311798163346273 ) ) ;
#50822=CARTESIAN_POINT ( 'NONE',  ( -3.318518101603030512, -7.321656987762886537, -6.254491282525755281E-15 ) ) ;
#51075=B_SPLINE_CURVE_WITH_KNOTS ( 'NONE', 3,
 ( #68107, #62472, #3385, #47308, #36088, #10039, #19913, #62115 ),
 .UNSPECIFIED., .F., .F.,
 ( 4, 2, 2, 4 ),
 ( 0.004673709593152176531, 0.005837709341827659881, 0.007001709090503144099, 0.009329708587854108198 ),
 .UNSPECIFIED. ) ;
#51308=CARTESIAN_POINT ( 'NONE',  ( 0.000000000000000000, 0.000000000000000000, -9.500000000000000000 ) ) ;
#51436=ORIENTED_EDGE ( 'NONE', *, *, #19719, .T. ) ;
#51680=DIRECTION ( 'NONE',  ( 0.000000000000000000, 0.000000000000000000, 1.000000000000000000 ) ) ;
#51868=DIRECTION ( 'NONE',  ( 0.000000000000000000, 0.000000000000000000, -1.000000000000000000 ) ) ;
#51884=CONICAL_SURFACE ( 'NONE', #41748, 8.000000000000001776, 1.047197551196595855 ) ;
#52234=CARTESIAN_POINT ( 'NONE',  ( 8.000000000000000000, 4.618802153517024500, -8.785468820183664818 ) ) ;
#52275=CARTESIAN_POINT ( 'NONE',  ( 0.000000000000000000, 0.000000000000000000, -9.500000000000000000 ) ) ;
#52518=DIRECTION ( 'NONE',  ( 0.5000000000000014433, 0.8660254037844379305, -0.000000000000000000 ) ) ;
#52636=VERTEX_POINT ( 'NONE', #63227 ) ;
#52794=ORIENTED_EDGE ( 'NONE', *, *, #46833, .T. ) ;
#52829=AXIS2_PLACEMENT_3D ( 'NONE', #55078, #16751, #22380 ) ;
#53054=CARTESIAN_POINT ( 'NONE',  ( 0.000000000000000000, 9.237604307034020579, -9.500000000000000000 ) ) ;
#53123=DIRECTION ( 'NONE',  ( 1.000000000000000000, 0.000000000000000000, 0.000000000000000000 ) ) ;
#53143=CARTESIAN_POINT ( 'NONE',  ( -0.6527133886630317461, 8.860760056385744932, -9.003039949738242953 ) ) ;
#53171=FACE_OUTER_BOUND ( 'NONE', #26953, .T. ) ;
#53217=CARTESIAN_POINT ( 'NONE',  ( -5.354491962338125965, 6.146186931204403514, -9.431901280394573206 ) ) ;
#53354=EDGE_LOOP ( 'NONE', ( #66472, #16755, #31196 ) ) ;
#53366=CARTESIAN_POINT ( 'NONE',  ( 8.000000000000001776, -0.7805016046291016751, -9.500000000000005329 ) ) ;
#53481=EDGE_CURVE ( 'NONE', #17325, #45082, #19405, .T. ) ;
#53547=PLANE ( 'NONE',  #62182 ) ;
#53664=EDGE_LOOP ( 'NONE', ( #30158, #9753 ) ) ;
#53704=EDGE_LOOP ( 'NONE', ( #61631, #2241, #53787, #64149 ) ) ;
#53787=ORIENTED_EDGE ( 'NONE', *, *, #5183, .T. ) ;
#53915=DIRECTION ( 'NONE',  ( 0.000000000000000000, 0.000000000000000000, 1.000000000000000000 ) ) ;
#53985=CONICAL_SURFACE ( 'NONE', #32667, 8.000000000000001776, 1.047197551196595855 ) ;
#54069=EDGE_CURVE ( 'NONE', #42836, #33757, #49517, .T. ) ;
#54145=CARTESIAN_POINT ( 'NONE',  ( -0.6527133886630325232, 8.860760056385744932, -0.4969600502617563254 ) ) ;
#54285=AXIS2_PLACEMENT_3D ( 'NONE', #26118, #4328, #25790 ) ;
#54293=ORIENTED_EDGE ( 'NONE', *, *, #22396, .F. ) ;
#54499=CARTESIAN_POINT ( 'NONE',  ( -2.644994884459115347, 7.710515798486364147, -0.08224679563971236396 ) ) ;
#54515=CARTESIAN_POINT ( 'NONE',  ( 4.000000000000011546, -6.928203230275505220, 0.000000000000000000 ) ) ;
#54840=VECTOR ( 'NONE', #66363, 1000.000000000000000 ) ;
#54873=ADVANCED_FACE ( 'NONE', ( #32114, #36354 ), #53547, .F. ) ;
#54912=CYLINDRICAL_SURFACE ( 'NONE', #61131, 5.000000000000000888 ) ;
#54997=ORIENTED_EDGE ( 'NONE', *, *, #3031, .T. ) ;
#55007=AXIS2_PLACEMENT_3D ( 'NONE', #47041, #57607, #24907 ) ;
#55024=CARTESIAN_POINT ( 'NONE',  ( -8.000000000000001776, 0.000000000000000000, 0.000000000000000000 ) ) ;
#55078=CARTESIAN_POINT ( 'NONE',  ( 0.000000000000000000, 0.000000000000000000, -0.5251556536572842271 ) ) ;
#55088=CARTESIAN_POINT ( 'NONE',  ( -8.000000000000000000, 0.000000000000000000, -9.500000000000000000 ) ) ;
#55163=EDGE_CURVE ( 'NONE', #69223, #21790, #7032, .T. ) ;
#55208=CARTESIAN_POINT ( 'NONE',  ( 8.000000000000001776, 0.000000000000000000, 0.000000000000000000 ) ) ;
#55268=CARTESIAN_POINT ( 'NONE',  ( 0.000000000000000000, 0.000000000000000000, -25.03750572909317285 ) ) ;
#55294=CARTESIAN_POINT ( 'NONE',  ( -5.354491962338131295, 6.146186931204402626, -0.06809871960542626668 ) ) ;
#55480=CARTESIAN_POINT ( 'NONE',  ( 0.000000000000000000, 0.000000000000000000, -0.5776712190230133270 ) ) ;
#55494=VECTOR ( 'NONE', #7270, 1000.000000000000000 ) ;
#55536=ADVANCED_FACE ( 'NONE', ( #46921 ), #36433, .T. ) ;
#55557=AXIS2_PLACEMENT_3D ( 'NONE', #62764, #42339, #63453 ) ;
#55709=CIRCLE ( 'NONE', #16383, 8.000000000000000000 ) ;
#56066=EDGE_CURVE ( 'NONE', #44487, #31187, #23394, .T. ) ;
#56351=ORIENTED_EDGE ( 'NONE', *, *, #21971, .F. ) ;
#56450=CARTESIAN_POINT ( 'NONE',  ( 0.000000000000000000, 0.000000000000000000, 0.000000000000000000 ) ) ;
#56515=B_SPLINE_CURVE_WITH_KNOTS ( 'NONE', 3,
 ( #68986, #63734, #15542, #26444, #36993, #31712, #53143, #47881 ),
 .UNSPECIFIED., .F., .F.,
 ( 4, 2, 2, 4 ),
 ( 0.004673709593152149643, 0.005837709341827642534, 0.007001709090503134558, 0.009329708587854118607 ),
 .UNSPECIFIED. ) ;
#56579=CARTESIAN_POINT ( 'NONE',  ( -8.000000000000000000, 4.618802153517024500, -8.785468820183664818 ) ) ;
#56693=VERTEX_POINT ( 'NONE', #66677 ) ;
#56791=CARTESIAN_POINT ( 'NONE',  ( 0.000000000000000000, 0.000000000000000000, -9.500000000000000000 ) ) ;
#56861=EDGE_CURVE ( 'NONE', #8652, #61707, #61936, .T. ) ;
#56925=AXIS2_PLACEMENT_3D ( 'NONE', #41064, #15364, #20290 ) ;
#57115=( NAMED_UNIT ( * ) PLANE_ANGLE_UNIT ( ) SI_UNIT ( $, .RADIAN. ) );
#57150=ORIENTED_EDGE ( 'NONE', *, *, #56066, .T. ) ;
#57217=DIRECTION ( 'NONE',  ( 1.000000000000000000, 0.000000000000000000, 0.000000000000000000 ) ) ;
#57263=DIRECTION ( 'NONE',  ( -0.000000000000000000, 0.000000000000000000, -1.000000000000000000 ) ) ;
#57387=FACE_OUTER_BOUND ( 'NONE', #45805, .T. ) ;
#57492=ADVANCED_FACE ( 'NONE', ( #29724 ), #59009, .T. ) ;
#57524=CARTESIAN_POINT ( 'NONE',  ( -6.183861102004804070E-16, 9.237604307034020579, -9.500000000000000000 ) ) ;
#57574=VERTEX_POINT ( 'NONE', #67036 ) ;
#57607=DIRECTION ( 'NONE',  ( 0.5000000000000014433, -0.8660254037844379305, 0.000000000000000000 ) ) ;
#57781=CARTESIAN_POINT ( 'NONE',  ( -8.000000000000000000, 4.618802153516996079, -9.500000000000000000 ) ) ;
#57790=CARTESIAN_POINT ( 'NONE',  ( 0.000000000000000000, 0.000000000000000000, -0.5251556536572842271 ) ) ;
#57833=CARTESIAN_POINT ( 'NONE',  ( -8.000000000000000000, 4.618802153517024500, -8.785468820183664818 ) ) ;
#57910=AXIS2_PLACEMENT_3D ( 'NONE', #55480, #43870, #38613 ) ;
#57948=ORIENTED_EDGE ( 'NONE', *, *, #22384, .T. ) ;
#58011=ORIENTED_EDGE ( 'NONE', *, *, #50575, .F. ) ;
#58090=VERTEX_POINT ( 'NONE', #14497 ) ;
#58194=EDGE_CURVE ( 'NONE', #59496, #1313, #55709, .T. ) ;
#58391=CARTESIAN_POINT ( 'NONE',  ( 0.000000000000000000, 0.000000000000000000, -9.500000000000000000 ) ) ;
#58409=DIRECTION ( 'NONE',  ( -0.000000000000000000, -0.000000000000000000, 1.000000000000000000 ) ) ;
#59009=CONICAL_SURFACE ( 'NONE', #5132, 8.000000000000001776, 1.047197551196595855 ) ;
#59297=ADVANCED_FACE ( 'NONE', ( #7664 ), #60105, .F. ) ;
#59415=ORIENTED_EDGE ( 'NONE', *, *, #61711, .T. ) ;
#59451=CARTESIAN_POINT ( 'NONE',  ( 4.681481898397010788, -6.534749472788160318, -5.187229768985335276E-15 ) ) ;
#59496=VERTEX_POINT ( 'NONE', #27493 ) ;
#59753=( NAMED_UNIT ( * ) PLANE_ANGLE_UNIT ( ) SI_UNIT ( $, .RADIAN. ) );
#59760=EDGE_CURVE ( 'NONE', #15636, #17325, #49290, .T. ) ;
#59776=CARTESIAN_POINT ( 'NONE',  ( -4.000000000000009770, -6.928203230275505220, -9.500000000000000000 ) ) ;
#59828=ORIENTED_EDGE ( 'NONE', *, *, #56066, .F. ) ;
#59896=EDGE_LOOP ( 'NONE', ( #33583, #22258, #6163, #28415, #22161, #63000 ) ) ;
#59909=AXIS2_PLACEMENT_3D ( 'NONE', #43611, #11595, #50299 ) ;
#59917=CARTESIAN_POINT ( 'NONE',  ( -8.000000000000000000, 0.000000000000000000, -9.500000000000000000 ) ) ;
#59996=MECHANICAL_DESIGN_GEOMETRIC_PRESENTATION_REPRESENTATION('',(#47488),#1618);
#60026=DIRECTION ( 'NONE',  ( -1.000000000000000000, 0.000000000000000000, 0.000000000000000000 ) ) ;
#60072=LINE ( 'NONE', #12251, #49051 ) ;
#60105=CONICAL_SURFACE ( 'NONE', #57910, 4.174999999999999822, 0.9599310885968758145 ) ;
#60140=CARTESIAN_POINT ( 'NONE',  ( -5.000000000000000888, 6.123233995736767268E-16, -9.500000000000000000 ) ) ;
#60274=CARTESIAN_POINT ( 'NONE',  ( 0.000000000000000000, 0.000000000000000000, -9.474599999999998801 ) ) ;
#60466=CARTESIAN_POINT ( 'NONE',  ( -0.6543471694412733575, -8.859816792613656844, -9.003584543331200507 ) ) ;
#60609=EDGE_LOOP ( 'NONE', ( #12511, #62761, #14585, #41825 ) ) ;
#60646=CARTESIAN_POINT ( 'NONE',  ( -8.000000000000000000, -1.555946510856147880, -9.432911297836646725 ) ) ;
#60721=CARTESIAN_POINT ( 'NONE',  ( -8.000000000000000000, 3.115336682267014989, -9.180606868608490956 ) ) ;
#61131=AXIS2_PLACEMENT_3D ( 'NONE', #55268, #38396, #21866 ) ;
#61283=CARTESIAN_POINT ( 'NONE',  ( -8.000000000000000000, -4.618802153517024500, -8.785468820183664818 ) ) ;
#61452=DIRECTION ( 'NONE',  ( -0.000000000000000000, -0.000000000000000000, 1.000000000000000000 ) ) ;
#61520=ORIENTED_EDGE ( 'NONE', *, *, #29557, .F. ) ;
#61619=CONICAL_SURFACE ( 'NONE', #27867, 5.000000000000000888, 0.9599310885968810325 ) ;
#61628=CARTESIAN_POINT ( 'NONE',  ( -5.355005115540906857, -6.145890662064668497, -9.417753204360275632 ) ) ;
#61631=ORIENTED_EDGE ( 'NONE', *, *, #47710, .F. ) ;
#61707=VERTEX_POINT ( 'NONE', #49660 ) ;
#61711=EDGE_CURVE ( 'NONE', #21790, #45082, #31485, .T. ) ;
#61760=CONICAL_SURFACE ( 'NONE', #14619, 8.000000000000001776, 1.047197551196595855 ) ;
#61823=CARTESIAN_POINT ( 'NONE',  ( 0.000000000000000000, 0.000000000000000000, 0.000000000000000000 ) ) ;
#61936=B_SPLINE_CURVE_WITH_KNOTS ( 'NONE', 3,
 ( #44057, #33538, #12419, #12067, #6443, #39494, #65538, #32476 ),
 .UNSPECIFIED., .F., .F.,
 ( 4, 2, 2, 4 ),
 ( 0.004673709593152176531, 0.005837709341827659881, 0.007001709090503144099, 0.009329708587854108198 ),
 .UNSPECIFIED. ) ;
#61987=CLOSED_SHELL ( 'NONE', ( #10205, #31397, #59297, #22226, #30590, #14367, #41460, #2181, #14034, #15329, #46337, #54873, #66885, #18583, #49533, #55536, #19230, #37699, #24870, #62246, #9745, #57492, #65441, #49115, #15959, #11836, #65794, #68679 ) ) ;
#62115=CARTESIAN_POINT ( 'NONE',  ( 8.000000000000000000, 4.618802153517024500, -0.7145311798163346273 ) ) ;
#62182=AXIS2_PLACEMENT_3D ( 'NONE', #5379, #21543, #42990 ) ;
#62234=EDGE_CURVE ( 'NONE', #31627, #44487, #3089, .T. ) ;
#62246=ADVANCED_FACE ( 'NONE', ( #9986 ), #37865, .T. ) ;
#62379=DIRECTION ( 'NONE',  ( 1.000000000000000000, 0.000000000000000000, 0.000000000000000000 ) ) ;
#62385=AXIS2_PLACEMENT_3D ( 'NONE', #19569, #10049, #3732 ) ;
#62389=DIRECTION ( 'NONE',  ( -0.8660254037844378194, 0.5000000000000013323, 0.000000000000000000 ) ) ;
#62416=CARTESIAN_POINT ( 'NONE',  ( 0.000000000000000000, 0.000000000000000000, 0.000000000000000000 ) ) ;
#62472=CARTESIAN_POINT ( 'NONE',  ( 4.339467034331195627, 6.732211846623388674, 5.929018872543287221E-15 ) ) ;
#62637=DIRECTION ( 'NONE',  ( -0.000000000000000000, -0.000000000000000000, 1.000000000000000000 ) ) ;
#62641=EDGE_CURVE ( 'NONE', #57574, #59496, #67500, .T. ) ;
#62761=ORIENTED_EDGE ( 'NONE', *, *, #30733, .F. ) ;
#62764=CARTESIAN_POINT ( 'NONE',  ( 0.000000000000000000, 0.000000000000000000, -9.500000000000000000 ) ) ;
#62769=CARTESIAN_POINT ( 'NONE',  ( -4.000000000000009770, -6.928203230275505220, 0.000000000000000000 ) ) ;
#62832=PRODUCT_CONTEXT ( 'NONE', #45758, 'mechanical' ) ;
#62884=EDGE_CURVE ( 'NONE', #44487, #33757, #23327, .T. ) ;
#63000=ORIENTED_EDGE ( 'NONE', *, *, #8511, .F. ) ;
#63016=ORIENTED_EDGE ( 'NONE', *, *, #21815, .T. ) ;
#63064=EDGE_LOOP ( 'NONE', ( #29071, #19733, #30132 ) ) ;
#63120=ORIENTED_EDGE ( 'NONE', *, *, #49564, .T. ) ;
#63227=CARTESIAN_POINT ( 'NONE',  ( -4.250000000000000000, 5.204748896376250699E-16, -8.949444346342716017 ) ) ;
#63315=B_SPLINE_CURVE_WITH_KNOTS ( 'NONE', 3,
 ( #57833, #21232, #20527, #53217, #10662, #26508 ),
 .UNSPECIFIED., .F., .F.,
 ( 4, 2, 4 ),
 ( 2.380731629708308052E-07, 0.002336973833157560305, 0.004673709593152149643 ),
 .UNSPECIFIED. ) ;
#63453=DIRECTION ( 'NONE',  ( 1.000000000000000000, 0.000000000000000000, 0.000000000000000000 ) ) ;
#63730=CARTESIAN_POINT ( 'NONE',  ( 0.000000000000000000, 0.000000000000000000, 0.000000000000000000 ) ) ;
#63734=CARTESIAN_POINT ( 'NONE',  ( -3.660532965668825245, 7.124194613927617326, -9.500000000000007105 ) ) ;
#63765=FILL_AREA_STYLE ('',( #27757 ) ) ;
#63778=VECTOR ( 'NONE', #35046, 1000.000000000000000 ) ;
#63782=EDGE_CURVE ( 'NONE', #10029, #47318, #56515, .T. ) ;
#63982=ORIENTED_EDGE ( 'NONE', *, *, #18850, .T. ) ;
#64088=CIRCLE ( 'NONE', #37120, 8.000000000000000000 ) ;
#64115=FACE_OUTER_BOUND ( 'NONE', #68950, .T. ) ;
#64137=PRODUCT_DEFINITION_SHAPE ( 'NONE', 'NONE',  #9991 ) ;
#64149=ORIENTED_EDGE ( 'NONE', *, *, #50575, .T. ) ;
#64436=ORIENTED_EDGE ( 'NONE', *, *, #11600, .T. ) ;
#64458=ORIENTED_EDGE ( 'NONE', *, *, #43355, .F. ) ;
#64573=CARTESIAN_POINT ( 'NONE',  ( 8.000000000000000000, -0.7805016046291005649, 1.033380195650246414E-15 ) ) ;
#64635=CARTESIAN_POINT ( 'NONE',  ( 8.000000000000003553, -4.618802153517020948, -8.785468820183664818 ) ) ;
#64717=DIRECTION ( 'NONE',  ( -1.000000000000000000, 0.000000000000000000, 0.000000000000000000 ) ) ;
#64744=CIRCLE ( 'NONE', #65875, 4.250000000000000000 ) ;
#64927=CARTESIAN_POINT ( 'NONE',  ( 8.000000000000001776, 0.000000000000000000, 0.000000000000000000 ) ) ;
#65054=SURFACE_SIDE_STYLE ('',( #15573 ) ) ;
#65105=ORIENTED_EDGE ( 'NONE', *, *, #42256, .F. ) ;
#65213=AXIS2_PLACEMENT_3D ( 'NONE', #7963, #12200, #13248 ) ;
#65251=CIRCLE ( 'NONE', #40545, 4.999999999999999112 ) ;
#65321=CARTESIAN_POINT ( 'NONE',  ( 0.000000000000000000, 0.000000000000000000, 0.000000000000000000 ) ) ;
#65441=ADVANCED_FACE ( 'NONE', ( #57387 ), #61760, .T. ) ;
#65538=CARTESIAN_POINT ( 'NONE',  ( 7.347286611336963702, 4.995646404165275278, -9.003039949738251835 ) ) ;
#65757=CARTESIAN_POINT ( 'NONE',  ( -3.816391647148975608E-14, -9.237604307034022355, -8.785468820183664818 ) ) ;
#65794=ADVANCED_FACE ( 'NONE', ( #40348 ), #15719, .F. ) ;
#65867=CARTESIAN_POINT ( 'NONE',  ( 4.999999999999999112, 0.000000000000000000, 3.469446951953614189E-15 ) ) ;
#65875=AXIS2_PLACEMENT_3D ( 'NONE', #25009, #45767, #35556 ) ;
#66075=DIRECTION ( 'NONE',  ( -0.000000000000000000, -0.000000000000000000, 1.000000000000000000 ) ) ;
#66285=CARTESIAN_POINT ( 'NONE',  ( 2.645508037661883360, 7.710219529346608702, -9.431901280394573206 ) ) ;
#66363=DIRECTION ( 'NONE',  ( -0.8191520442889916875, 0.000000000000000000, -0.5735764363510462704 ) ) ;
#66399=CARTESIAN_POINT ( 'NONE',  ( -8.000000000000000000, -4.618802153517023612, -9.500000000000000000 ) ) ;
#66432=CONICAL_SURFACE ( 'NONE', #68649, 8.000000000000001776, 1.047197551196595855 ) ;
#66472=ORIENTED_EDGE ( 'NONE', *, *, #19769, .T. ) ;
#66634=CARTESIAN_POINT ( 'NONE',  ( -8.000000000000000000, -4.618802153517024500, -8.785468820183664818 ) ) ;
#66677=CARTESIAN_POINT ( 'NONE',  ( 5.000000000000000888, 0.000000000000000000, -9.500000000000000000 ) ) ;
#66700=ORIENTED_EDGE ( 'NONE', *, *, #20562, .T. ) ;
#66745=LINE ( 'NONE', #66399, #37957 ) ;
#66747=ORIENTED_EDGE ( 'NONE', *, *, #20562, .F. ) ;
#66775=VERTEX_POINT ( 'NONE', #14413 ) ;
#66832=AXIS2_PLACEMENT_3D ( 'NONE', #50530, #44558, #8319 ) ;
#66882=EDGE_LOOP ( 'NONE', ( #43111, #29380, #4147, #11081 ) ) ;
#66885=ADVANCED_FACE ( 'NONE', ( #13375, #34838 ), #13711, .T. ) ;
#66950=ORIENTED_EDGE ( 'NONE', *, *, #26983, .T. ) ;
#66984=CARTESIAN_POINT ( 'NONE',  ( 2.645508037661883360, 7.710219529346608702, -0.06809871960542647484 ) ) ;
#67036=CARTESIAN_POINT ( 'NONE',  ( 8.000000000000003553, -4.618802153517020948, -0.7145311798163346273 ) ) ;
#67064=AXIS2_PLACEMENT_3D ( 'NONE', #57781, #34693, #9595 ) ;
#67169=CARTESIAN_POINT ( 'NONE',  ( 8.000000000000000000, 4.618802153517024500, -0.7145311798163346273 ) ) ;
#67500=B_SPLINE_CURVE_WITH_KNOTS ( 'NONE', 3,
 ( #12157, #43104, #43791, #48712, #64573, #64927 ),
 .UNSPECIFIED., .F., .F.,
 ( 4, 2, 4 ),
 ( 0.008240550023493531037, 0.01057684187039406240, 0.01291313371729459203 ),
 .UNSPECIFIED. ) ;
#67690=DIRECTION ( 'NONE',  ( -1.000000000000000000, 0.000000000000000000, 0.000000000000000000 ) ) ;
#67844=ORIENTED_EDGE ( 'NONE', *, *, #62884, .F. ) ;
#67899=ORIENTED_EDGE ( 'NONE', *, *, #21731, .T. ) ;
#68088=CARTESIAN_POINT ( 'NONE',  ( 8.000000000000000000, 0.7809653281576076633, -9.500000000000001776 ) ) ;
#68107=CARTESIAN_POINT ( 'NONE',  ( 4.000000000000012434, 6.928203230275504332, 0.000000000000000000 ) ) ;
#68121=ORIENTED_EDGE ( 'NONE', *, *, #126, .T. ) ;
#68250=AXIS2_PLACEMENT_3D ( 'NONE', #48180, #49225, #15844 ) ;
#68277=ORIENTED_EDGE ( 'NONE', *, *, #38257, .F. ) ;
#68436=EDGE_LOOP ( 'NONE', ( #64436, #37288, #29621 ) ) ;
#68479=EDGE_LOOP ( 'NONE', ( #66700, #51436, #63982, #15135, #8250, #45695 ) ) ;
#68649=AXIS2_PLACEMENT_3D ( 'NONE', #52275, #61452, #57217 ) ;
#68679=ADVANCED_FACE ( 'NONE', ( #22568 ), #54912, .F. ) ;
#68714=DIRECTION ( 'NONE',  ( 0.000000000000000000, 0.000000000000000000, -1.000000000000000000 ) ) ;
#68730=CARTESIAN_POINT ( 'NONE',  ( -4.000000000000013323, 6.928203230275504332, -9.500000000000000000 ) ) ;
#68877=B_SPLINE_CURVE_WITH_KNOTS ( 'NONE', 3,
 ( #2669, #68088, #19888, #9328, #30789, #52234 ),
 .UNSPECIFIED., .F., .F.,
 ( 4, 2, 4 ),
 ( 0.01291313371729459550, 0.01525081363757311605, 0.01758849355785163660 ),
 .UNSPECIFIED. ) ;
#68950=EDGE_LOOP ( 'NONE', ( #41761, #3927, #18584 ) ) ;
#68986=CARTESIAN_POINT ( 'NONE',  ( -4.000000000000013323, 6.928203230275504332, -9.500000000000000000 ) ) ;
#69223=VERTEX_POINT ( 'NONE', #56579 ) ;
#69290=AXIS2_PLACEMENT_3D ( 'NONE', #49277, #10964, #27483 ) ;
ENDSEC;
END-ISO-10303-21;
